ISO-10303-21;
HEADER;
FILE_DESCRIPTION (('STEP AP203'),
    '1' );
FILE_NAME ('bench vise2-.step',
    '2026-10-07T23:37:23',
    ( '' ),
    ( '' ),
    'SwSTEP 2.0',
    'SolidWorks 2024',
    '' );
FILE_SCHEMA (( 'AUTOMOTIVE_DESIGN' ));
ENDSEC;

DATA;
#1=EDGE_CURVE ( 'NONE', #6151, #2183, #1599, .T. ) ;
#5=ORIENTED_EDGE ( 'NONE', *, *, #5735, .T. ) ;
#7=CARTESIAN_POINT ( 'NONE',  ( 2.537500000000000533, 2.500000000000000444, 0.2625000000000008438 ) ) ;
#8=ADVANCED_FACE ( 'NONE', ( #7344 ), #2858, .F. ) ;
#11=CARTESIAN_POINT ( 'NONE',  ( -0.7335700379171464780, 2.500000000182677873, -2.908930215554831999 ) ) ;
#13=ADVANCED_FACE ( 'NONE', ( #7172 ), #6014, .F. ) ;
#14=AXIS2_PLACEMENT_3D ( 'NONE', #1376, #7034, #673 ) ;
#15=CYLINDRICAL_SURFACE ( 'NONE', #5940, 2.841000000000000636 ) ;
#18=LINE ( 'NONE', #3837, #1501 ) ;
#19=EDGE_CURVE ( 'NONE', #3352, #6547, #5345, .T. ) ;
#23=DIRECTION ( 'NONE',  ( 0.000000000000000000, 0.000000000000000000, 1.000000000000000000 ) ) ;
#24=AXIS2_PLACEMENT_3D ( 'NONE', #1125, #5495, #3538 ) ;
#27=LINE ( 'NONE', #5041, #2456 ) ;
#30=ORIENTED_EDGE ( 'NONE', *, *, #1937, .F. ) ;
#32=AXIS2_PLACEMENT_3D ( 'NONE', #473, #3002, #4187 ) ;
#34=AXIS2_PLACEMENT_3D ( 'NONE', #7877, #946, #1033 ) ;
#36=ADVANCED_FACE ( 'NONE', ( #6211 ), #602, .T. ) ;
#37=CARTESIAN_POINT ( 'NONE',  ( -0.5082965702588324586, 2.405310912759768716, -3.001266468626919259 ) ) ;
#38=CARTESIAN_POINT ( 'NONE',  ( 0.8670765961576291092, 4.936241069566050577, -5.108749999999999680 ) ) ;
#42=ADVANCED_FACE ( 'NONE', ( #1382 ), #6295, .T. ) ;
#47=VERTEX_POINT ( 'NONE', #5759 ) ;
#59=CARTESIAN_POINT ( 'NONE',  ( 1.625000000000000222, 5.113999999999999879, -2.750000000000000444 ) ) ;
#62=EDGE_CURVE ( 'NONE', #2284, #7136, #4477, .T. ) ;
#77=CARTESIAN_POINT ( 'NONE',  ( 0.000000000000000000, 3.950000000000000178, 2.749999999536766992 ) ) ;
#78=EDGE_CURVE ( 'NONE', #6387, #3627, #5164, .T. ) ;
#83=DIRECTION ( 'NONE',  ( 1.000000000000000000, 0.000000000000000000, 0.000000000000000000 ) ) ;
#84=CARTESIAN_POINT ( 'NONE',  ( -0.001186137648316157355, 2.637500537863615158, -5.108750000000001457 ) ) ;
#90=ORIENTED_EDGE ( 'NONE', *, *, #3285, .F. ) ;
#91=CARTESIAN_POINT ( 'NONE',  ( 0.000000000000000000, 3.950000000000000178, -5.108750000000001457 ) ) ;
#95=VERTEX_POINT ( 'NONE', #3821 ) ;
#99=CARTESIAN_POINT ( 'NONE',  ( -1.489119986720869093, 2.223645902163796428, 2.750000000000000444 ) ) ;
#103=CARTESIAN_POINT ( 'NONE',  ( 0.000000000000000000, 1.664000000000000368, 2.693920355039552791E-42 ) ) ;
#104=CARTESIAN_POINT ( 'NONE',  ( 1.312500000000000444, 8.589000000000002188, 3.161250000147724837 ) ) ;
#106=ORIENTED_EDGE ( 'NONE', *, *, #5767, .F. ) ;
#112=CARTESIAN_POINT ( 'NONE',  ( -2.750000000000000444, 8.601278779527561369, 3.691250000000001030 ) ) ;
#113=EDGE_CURVE ( 'NONE', #6547, #6766, #6910, .T. ) ;
#118=ADVANCED_FACE ( 'NONE', ( #182 ), #7038, .F. ) ;
#121=DIRECTION ( 'NONE',  ( 0.000000000000000000, -1.000000000000000000, 0.000000000000000000 ) ) ;
#122=CARTESIAN_POINT ( 'NONE',  ( 1.282759084805754402, 3.671339687942380525, -5.108750000000001457 ) ) ;
#123=CARTESIAN_POINT ( 'NONE',  ( 0.7335700383277801162, 2.500000000390421473, -2.908930215353081383 ) ) ;
#124=DIRECTION ( 'NONE',  ( 1.000000000000000000, 0.000000000000000000, 0.000000000000000000 ) ) ;
#126=CARTESIAN_POINT ( 'NONE',  ( 1.624999999336056655, 2.076218727025485933, 2.749999998825987557 ) ) ;
#127=B_SPLINE_CURVE_WITH_KNOTS ( 'NONE', 3,
 ( #126, #2024, #4520, #1417, #2983, #7595 ),
 .UNSPECIFIED., .F., .F.,
 ( 4, 2, 4 ),
 ( 0.000000000000000000, 0.007631658709671237072, 0.01526331741934247414 ),
 .UNSPECIFIED. ) ;
#130=DIRECTION ( 'NONE',  ( -0.000000000000000000, 1.000000000000000000, -0.000000000000000000 ) ) ;
#131=DIRECTION ( 'NONE',  ( -0.000000000000000000, -0.000000000000000000, 1.000000000000000000 ) ) ;
#133=DIRECTION ( 'NONE',  ( -0.000000000000000000, -0.000000000000000000, 1.000000000000000000 ) ) ;
#139=CARTESIAN_POINT ( 'NONE',  ( -1.347488132528783966, 2.365290550993251806, 2.750000000000000444 ) ) ;
#150=PLANE ( 'NONE',  #5416 ) ;
#156=CARTESIAN_POINT ( 'NONE',  ( -2.750000000000000888, 8.574153543307089009, 3.323750000000001315 ) ) ;
#158=ORIENTED_EDGE ( 'NONE', *, *, #3778, .F. ) ;
#159=FACE_OUTER_BOUND ( 'NONE', #7228, .T. ) ;
#161=ORIENTED_EDGE ( 'NONE', *, *, #1, .T. ) ;
#162=EDGE_CURVE ( 'NONE', #7663, #2678, #722, .T. ) ;
#163=VECTOR ( 'NONE', #263, 39.37007874015748143 ) ;
#164=VECTOR ( 'NONE', #2503, 39.37007874015748143 ) ;
#168=CARTESIAN_POINT ( 'NONE',  ( 0.001186118861278498285, 5.262499470843738258, -5.108750000000001457 ) ) ;
#170=ORIENTED_EDGE ( 'NONE', *, *, #1035, .F. ) ;
#176=AXIS2_PLACEMENT_3D ( 'NONE', #828, #121, #3331 ) ;
#177=EDGE_CURVE ( 'NONE', #1721, #1286, #2037, .T. ) ;
#179=VECTOR ( 'NONE', #3445, 39.37007874015748143 ) ;
#182=FACE_OUTER_BOUND ( 'NONE', #740, .T. ) ;
#189=CARTESIAN_POINT ( 'NONE',  ( -2.078417272059708142E-11, 5.113999999999999879, 2.749999998413802160 ) ) ;
#190=ADVANCED_FACE ( 'NONE', ( #1297 ), #3855, .T. ) ;
#195=AXIS2_PLACEMENT_3D ( 'NONE', #5137, #2034, #1912 ) ;
#205=AXIS2_PLACEMENT_3D ( 'NONE', #3133, #8065, #544 ) ;
#206=PLANE ( 'NONE',  #2136 ) ;
#207=DIRECTION ( 'NONE',  ( 0.000000000000000000, 0.000000000000000000, 1.000000000000000000 ) ) ;
#208=CARTESIAN_POINT ( 'NONE',  ( -2.750000000000000444, 8.589000000000000412, 2.411250000000000338 ) ) ;
#209=FACE_OUTER_BOUND ( 'NONE', #5642, .T. ) ;
#216=EDGE_CURVE ( 'NONE', #5858, #3882, #4440, .T. ) ;
#222=EDGE_LOOP ( 'NONE', ( #1976, #4113, #505 ) ) ;
#225=CARTESIAN_POINT ( 'NONE',  ( 1.624999999336056655, 2.076218727025485933, 2.749999998825987557 ) ) ;
#227=AXIS2_PLACEMENT_3D ( 'NONE', #112, #741, #2627 ) ;
#228=EDGE_CURVE ( 'NONE', #1632, #6240, #2956, .T. ) ;
#238=DIRECTION ( 'NONE',  ( 0.000000000000000000, 0.000000000000000000, -1.000000000000000000 ) ) ;
#249=EDGE_CURVE ( 'NONE', #3378, #2362, #5077, .T. ) ;
#250=CARTESIAN_POINT ( 'NONE',  ( 1.625000000000000222, 5.639000000000001123, 0.1249999999999998057 ) ) ;
#251=CARTESIAN_POINT ( 'NONE',  ( -1.213899175414482112, 4.454554504762766598, -5.108749999999998792 ) ) ;
#253=CARTESIAN_POINT ( 'NONE',  ( 2.537500000000000533, 1.664000000000000368, 0.2625000000000008438 ) ) ;
#256=ORIENTED_EDGE ( 'NONE', *, *, #6787, .T. ) ;
#259=CYLINDRICAL_SURFACE ( 'NONE', #8003, 2.841000000000000636 ) ;
#263=DIRECTION ( 'NONE',  ( 1.000000000000000000, 0.000000000000000000, 0.000000000000000000 ) ) ;
#264=CARTESIAN_POINT ( 'NONE',  ( 2.187663376927555706E-18, 3.950000000000000178, 0.1249999999999999029 ) ) ;
#265=CARTESIAN_POINT ( 'NONE',  ( 1.312500000000000444, 5.414000000000000590, 0.5414159055118111796 ) ) ;
#266=VERTEX_POINT ( 'NONE', #3033 ) ;
#268=CARTESIAN_POINT ( 'NONE',  ( 0.06610591232966753217, 2.325000000000000622, -3.080208333333334547 ) ) ;
#273=CARTESIAN_POINT ( 'NONE',  ( 3.479221556377631263E-16, 1.664000000000000368, -2.841000000000000636 ) ) ;
#277=VERTEX_POINT ( 'NONE', #7 ) ;
#278=DIRECTION ( 'NONE',  ( 0.000000000000000000, -1.000000000000000000, 0.000000000000000000 ) ) ;
#279=EDGE_CURVE ( 'NONE', #1945, #6623, #5961, .T. ) ;
#281=ORIENTED_EDGE ( 'NONE', *, *, #1606, .T. ) ;
#283=ORIENTED_EDGE ( 'NONE', *, *, #4235, .F. ) ;
#288=CARTESIAN_POINT ( 'NONE',  ( -1.178157499656855345, 3.371148463989271260, -5.108749999999998792 ) ) ;
#289=CARTESIAN_POINT ( 'NONE',  ( 0.6236586488130037020, 2.448156299858527785, 2.959379238582043659 ) ) ;
#290=CARTESIAN_POINT ( 'NONE',  ( 3.296097360985625002, 1.750000000000000444, 0.5624999982029994516 ) ) ;
#292=CARTESIAN_POINT ( 'NONE',  ( 1.500000000000000444, 5.414000000000000590, -2.750000000000000444 ) ) ;
#293=ORIENTED_EDGE ( 'NONE', *, *, #7524, .T. ) ;
#304=CARTESIAN_POINT ( 'NONE',  ( 1.624999999999999556, 2.076218724953421191, -2.749999999536766992 ) ) ;
#306=DIRECTION ( 'NONE',  ( 1.000000000000000000, 0.000000000000000000, 0.000000000000000000 ) ) ;
#309=VECTOR ( 'NONE', #4716, 39.37007874015748143 ) ;
#314=AXIS2_PLACEMENT_3D ( 'NONE', #4341, #6848, #4999 ) ;
#319=EDGE_LOOP ( 'NONE', ( #3487, #7771, #920, #3756, #8180, #5464, #8111, #680 ) ) ;
#321=ORIENTED_EDGE ( 'NONE', *, *, #4235, .T. ) ;
#328=AXIS2_PLACEMENT_3D ( 'NONE', #4120, #1026, #2896 ) ;
#329=CARTESIAN_POINT ( 'NONE',  ( -1.042238299988425876, 4.752397365051017175, -5.108749999999998792 ) ) ;
#331=DIRECTION ( 'NONE',  ( -1.000000000000000000, 0.000000000000000000, -0.000000000000000000 ) ) ;
#332=CARTESIAN_POINT ( 'NONE',  ( -1.312500000000000888, 7.339000000000001300, 3.161250000000001670 ) ) ;
#333=EDGE_CURVE ( 'NONE', #3882, #4495, #4768, .T. ) ;
#337=EDGE_CURVE ( 'NONE', #691, #1844, #2028, .T. ) ;
#340=LINE ( 'NONE', #2844, #5652 ) ;
#341=EDGE_LOOP ( 'NONE', ( #1611, #8073, #1909, #7362 ) ) ;
#343=PLANE ( 'NONE',  #5809 ) ;
#344=DIRECTION ( 'NONE',  ( -0.000000000000000000, 0.000000000000000000, -1.000000000000000000 ) ) ;
#346=VECTOR ( 'NONE', #4353, 39.37007874015748143 ) ;
#347=DIRECTION ( 'NONE',  ( -0.000000000000000000, -0.000000000000000000, 1.000000000000000000 ) ) ;
#353=DIRECTION ( 'NONE',  ( 1.000000000000000000, 0.000000000000000000, -0.000000000000000000 ) ) ;
#356=CARTESIAN_POINT ( 'NONE',  ( 0.000000000000000000, 1.664000000000000368, 2.693920355039552791E-42 ) ) ;
#357=CARTESIAN_POINT ( 'NONE',  ( 1.625000000000000222, 2.359134605023787579, -2.598586947582201656 ) ) ;
#359=ORIENTED_EDGE ( 'NONE', *, *, #4589, .F. ) ;
#366=ADVANCED_FACE ( 'NONE', ( #3003, #3097 ), #6245, .T. ) ;
#367=CARTESIAN_POINT ( 'NONE',  ( -0.08777340432027264105, 2.639721318438408293, -5.108750000000001457 ) ) ;
#368=CARTESIAN_POINT ( 'NONE',  ( 0.7335700383901263555, 2.500000000202698303, 2.908930215426092758 ) ) ;
#379=EDGE_CURVE ( 'NONE', #7238, #5748, #5501, .T. ) ;
#387=CARTESIAN_POINT ( 'NONE',  ( -1.624999999336056877, 2.076218724820237060, -2.750000000000000444 ) ) ;
#395=CARTESIAN_POINT ( 'NONE',  ( 0.000000000000000000, 3.950000000000000178, -2.750000000000000444 ) ) ;
#398=ADVANCED_FACE ( 'NONE', ( #6858 ), #4513, .T. ) ;
#399=CARTESIAN_POINT ( 'NONE',  ( 1.562500000000000444, 5.639000000000001123, -2.908930215307243383 ) ) ;
#404=LINE ( 'NONE', #3357, #5288 ) ;
#407=ORIENTED_EDGE ( 'NONE', *, *, #6294, .T. ) ;
#408=CARTESIAN_POINT ( 'NONE',  ( 2.750000000000000444, 7.964000000000000412, 3.323750000000001759 ) ) ;
#409=DIRECTION ( 'NONE',  ( 0.000000000000000000, -0.000000000000000000, 1.000000000000000000 ) ) ;
#412=DIRECTION ( 'NONE',  ( 1.000000000000000000, -0.000000000000000000, 0.000000000000000000 ) ) ;
#413=CARTESIAN_POINT ( 'NONE',  ( -2.537500000000000533, 1.664000000000000368, 0.000000000000000000 ) ) ;
#414=CARTESIAN_POINT ( 'NONE',  ( 2.750000000000000444, 7.521783346456695440, 3.691250000000001030 ) ) ;
#417=VERTEX_POINT ( 'NONE', #2519 ) ;
#421=FACE_BOUND ( 'NONE', #5161, .T. ) ;
#424=ORIENTED_EDGE ( 'NONE', *, *, #4346, .T. ) ;
#429=ORIENTED_EDGE ( 'NONE', *, *, #735, .T. ) ;
#439=EDGE_LOOP ( 'NONE', ( #407, #3359, #4905, #2556, #2069, #7406 ) ) ;
#444=CARTESIAN_POINT ( 'NONE',  ( -1.312500000000000444, 5.414000000000000590, 2.749999994424771721 ) ) ;
#445=VERTEX_POINT ( 'NONE', #3209 ) ;
#448=VECTOR ( 'NONE', #2131, 39.37007874015748143 ) ;
#450=DIRECTION ( 'NONE',  ( -1.000000000000000000, 0.000000000000000000, -0.000000000000000000 ) ) ;
#452=AXIS2_PLACEMENT_3D ( 'NONE', #1842, #1114, #5485 ) ;
#454=VECTOR ( 'NONE', #2553, 39.37007874015748143 ) ;
#460=AXIS2_PLACEMENT_3D ( 'NONE', #1459, #6463, #6417 ) ;
#461=CARTESIAN_POINT ( 'NONE',  ( 1.625000000000000222, 5.339000000000000412, 0.1249999999999998057 ) ) ;
#469=ORIENTED_EDGE ( 'NONE', *, *, #1930, .T. ) ;
#471=DIRECTION ( 'NONE',  ( -0.000000000000000000, 0.000000000000000000, -1.000000000000000000 ) ) ;
#473=CARTESIAN_POINT ( 'NONE',  ( 0.000000000000000000, 2.500000000000000000, 0.000000000000000000 ) ) ;
#477=DIRECTION ( 'NONE',  ( -0.000000000000000000, 1.000000000000000000, 0.000000000000000000 ) ) ;
#478=ORIENTED_EDGE ( 'NONE', *, *, #3819, .F. ) ;
#480=VECTOR ( 'NONE', #2249, 39.37007874015748143 ) ;
#482=CIRCLE ( 'NONE', #7583, 1.624999999999999778 ) ;
#487=ADVANCED_FACE ( 'NONE', ( #7111 ), #3250, .T. ) ;
#488=DIRECTION ( 'NONE',  ( -0.000000000000000000, 1.000000000000000000, 0.000000000000000000 ) ) ;
#489=DIRECTION ( 'NONE',  ( -0.000000000000000000, 1.000000000000000000, -0.000000000000000000 ) ) ;
#490=EDGE_LOOP ( 'NONE', ( #7515, #2757 ) ) ;
#498=MECHANICAL_CONTEXT ( 'NONE', #4403, 'mechanical' ) ;
#505=ORIENTED_EDGE ( 'NONE', *, *, #5505, .F. ) ;
#514=CARTESIAN_POINT ( 'NONE',  ( 0.000000000000000000, 5.339000000000000412, -2.750000000000000444 ) ) ;
#518=DIRECTION ( 'NONE',  ( 1.000000000000000000, 0.000000000000000000, 0.000000000000000000 ) ) ;
#523=DIRECTION ( 'NONE',  ( -0.000000000000000000, -0.000000000000000000, 1.000000000000000000 ) ) ;
#530=LINE ( 'NONE', #1811, #3472 ) ;
#536=CARTESIAN_POINT ( 'NONE',  ( -3.296097361031207207, 1.750000000037170489, -0.5624999991015005030 ) ) ;
#540=VERTEX_POINT ( 'NONE', #4559 ) ;
#542=CARTESIAN_POINT ( 'NONE',  ( 0.04795090551181103306, 5.268934960629921171, -5.098161062992129011 ) ) ;
#544=DIRECTION ( 'NONE',  ( 0.000000000000000000, 0.000000000000000000, -1.000000000000000000 ) ) ;
#547=CARTESIAN_POINT ( 'NONE',  ( 0.001186118861278498285, 5.262499470843738258, -5.108750000000001457 ) ) ;
#548=EDGE_CURVE ( 'NONE', #2064, #1699, #5704, .T. ) ;
#553=CARTESIAN_POINT ( 'NONE',  ( 1.624999999336056655, 2.076218727025485933, 2.749999998825987557 ) ) ;
#560=VECTOR ( 'NONE', #891, 39.37007874015748143 ) ;
#564=CARTESIAN_POINT ( 'NONE',  ( 2.537500000000000533, 1.664000000000000368, 0.000000000000000000 ) ) ;
#569=DIRECTION ( 'NONE',  ( 1.000000000000000000, 0.000000000000000000, -0.000000000000000000 ) ) ;
#573=ORIENTED_EDGE ( 'NONE', *, *, #4497, .F. ) ;
#575=PLANE ( 'NONE',  #8140 ) ;
#585=CIRCLE ( 'NONE', #4097, 1.624999999999999778 ) ;
#592=CARTESIAN_POINT ( 'NONE',  ( 0.000000000000000000, 3.950000000000000178, -4.308749999765625560 ) ) ;
#593=LINE ( 'NONE', #4890, #698 ) ;
#594=CARTESIAN_POINT ( 'NONE',  ( -1.994041535433071610, 4.020147637795276729, -4.886192834645670224 ) ) ;
#597=ORIENTED_EDGE ( 'NONE', *, *, #4661, .F. ) ;
#599=DIRECTION ( 'NONE',  ( 1.000000000000000000, 0.000000000000000000, -0.000000000000000000 ) ) ;
#602=PLANE ( 'NONE',  #6628 ) ;
#604=CARTESIAN_POINT ( 'NONE',  ( 1.500000000000000444, 3.950000000000000178, 2.750000000234376074 ) ) ;
#608=CARTESIAN_POINT ( 'NONE',  ( -3.343750000000001776, 1.750000000000000444, 3.383875000000000632 ) ) ;
#610=DIRECTION ( 'NONE',  ( 0.000000000000000000, 0.000000000000000000, 1.000000000000000000 ) ) ;
#614=CARTESIAN_POINT ( 'NONE',  ( -1.625000000000000222, 5.339000000000000412, -2.750000000000000444 ) ) ;
#618=LINE ( 'NONE', #7455, #2288 ) ;
#627=DIRECTION ( 'NONE',  ( 1.000000000000000000, 0.000000000000000000, 0.000000000000000000 ) ) ;
#633=CARTESIAN_POINT ( 'NONE',  ( -0.3234663987973003807, 2.357191439933449040, -3.048510081330109589 ) ) ;
#634=CARTESIAN_POINT ( 'NONE',  ( 1.042238314306938918, 3.147602674133755496, -5.108750000000002345 ) ) ;
#640=ORIENTED_EDGE ( 'NONE', *, *, #3833, .F. ) ;
#642=DIRECTION ( 'NONE',  ( 0.000000000000000000, 1.000000000000000000, -0.000000000000000000 ) ) ;
#644=PLANE ( 'NONE',  #5989 ) ;
#653=EDGE_LOOP ( 'NONE', ( #6266, #7461, #5848, #1274 ) ) ;
#655=CARTESIAN_POINT ( 'NONE',  ( 1.624999999999999778, 3.950000000000000178, 3.691250000234376216 ) ) ;
#657=EDGE_LOOP ( 'NONE', ( #1299, #2971, #6391, #5149 ) ) ;
#663=DIRECTION ( 'NONE',  ( 0.000000000000000000, -0.000000000000000000, 1.000000000000000000 ) ) ;
#665=ORIENTED_EDGE ( 'NONE', *, *, #7096, .T. ) ;
#667=DIRECTION ( 'NONE',  ( 0.000000000000000000, 1.000000000000000000, -0.000000000000000000 ) ) ;
#668=CARTESIAN_POINT ( 'NONE',  ( 1.168432146579409636, 4.548236705813060610, -5.108749999999999680 ) ) ;
#673=DIRECTION ( 'NONE',  ( 1.000000000000000000, 0.000000000000000000, 0.000000000000000000 ) ) ;
#674=VERTEX_POINT ( 'NONE', #1698 ) ;
#676=CARTESIAN_POINT ( 'NONE',  ( -2.750000000000000444, 7.964000000000001300, 3.323750000000001759 ) ) ;
#680=ORIENTED_EDGE ( 'NONE', *, *, #1941, .T. ) ;
#682=DIRECTION ( 'NONE',  ( -1.000000000000000000, 0.000000000000000000, 0.000000000000000000 ) ) ;
#691=VERTEX_POINT ( 'NONE', #387 ) ;
#692=DIRECTION ( 'NONE',  ( -1.000000000000000000, 0.000000000000000000, 0.000000000000000000 ) ) ;
#698=VECTOR ( 'NONE', #4968, 39.37007874015748143 ) ;
#709=VECTOR ( 'NONE', #7101, 39.37007874015748143 ) ;
#710=CIRCLE ( 'NONE', #5820, 0.2625000000000008438 ) ;
#713=CARTESIAN_POINT ( 'NONE',  ( 0.3381868679734887362, 2.681086572149180558, -5.108749999999998792 ) ) ;
#716=CARTESIAN_POINT ( 'NONE',  ( 2.537500000000000533, 2.500000000000000444, 0.2625000000000008438 ) ) ;
#722=LINE ( 'NONE', #3216, #3349 ) ;
#725=EDGE_LOOP ( 'NONE', ( #1151, #6212, #424, #2408, #7036, #1194, #6828, #2931, #7258 ) ) ;
#730=EDGE_CURVE ( 'NONE', #4783, #1844, #6554, .T. ) ;
#733=LINE ( 'NONE', #5731, #5536 ) ;
#734=DIRECTION ( 'NONE',  ( 1.000000000000000000, 0.000000000000000000, 0.000000000000000000 ) ) ;
#735=EDGE_CURVE ( 'NONE', #2183, #7519, #5964, .T. ) ;
#740=EDGE_LOOP ( 'NONE', ( #4028, #158, #2090, #3946 ) ) ;
#741=DIRECTION ( 'NONE',  ( 1.000000000000000000, 0.000000000000000000, 0.000000000000000000 ) ) ;
#744=VECTOR ( 'NONE', #2267, 39.37007874015748143 ) ;
#746=DIRECTION ( 'NONE',  ( -0.000000000000000000, -1.000000000000000000, 0.000000000000000000 ) ) ;
#748=DIRECTION ( 'NONE',  ( -0.000000000000000000, -1.000000000000000000, -0.000000000000000000 ) ) ;
#752=ORIENTED_EDGE ( 'NONE', *, *, #3749, .F. ) ;
#755=CARTESIAN_POINT ( 'NONE',  ( 1.178157500071308261, 4.528851530234832445, -5.108750000000001457 ) ) ;
#756=DIRECTION ( 'NONE',  ( -0.000000000000000000, -0.000000000000000000, 1.000000000000000000 ) ) ;
#761=DIRECTION ( 'NONE',  ( 0.000000000000000000, 0.000000000000000000, 1.000000000000000000 ) ) ;
#762=ORIENTED_EDGE ( 'NONE', *, *, #7780, .T. ) ;
#764=DIRECTION ( 'NONE',  ( 0.000000000000000000, 0.000000000000000000, 1.000000000000000000 ) ) ;
#772=LINE ( 'NONE', #6958, #7989 ) ;
#777=ORIENTED_EDGE ( 'NONE', *, *, #6886, .T. ) ;
#781=ADVANCED_FACE ( 'NONE', ( #2884 ), #2847, .F. ) ;
#783=ORIENTED_EDGE ( 'NONE', *, *, #1105, .F. ) ;
#786=LINE ( 'NONE', #6934, #709 ) ;
#791=EDGE_CURVE ( 'NONE', #7238, #4179, #7927, .T. ) ;
#792=CARTESIAN_POINT ( 'NONE',  ( 1.138021836555352051, 4.605302133062858516, -5.108749999999999680 ) ) ;
#793=ORIENTED_EDGE ( 'NONE', *, *, #5886, .T. ) ;
#796=DIRECTION ( 'NONE',  ( -0.000000000000000000, -1.000000000000000000, 0.000000000000000000 ) ) ;
#800=CARTESIAN_POINT ( 'NONE',  ( 0.000000000000000000, 1.664000000000000368, 2.841000000000000636 ) ) ;
#804=CARTESIAN_POINT ( 'NONE',  ( 0.000000000000000000, 5.339000000000000412, 0.1249999999999997641 ) ) ;
#807=DIRECTION ( 'NONE',  ( 0.000000000000000000, 0.000000000000000000, 1.000000000000000000 ) ) ;
#811=VERTEX_POINT ( 'NONE', #3585 ) ;
#818=CARTESIAN_POINT ( 'NONE',  ( 0.000000000000000000, 1.750000000000000444, 2.841000000000000636 ) ) ;
#827=VECTOR ( 'NONE', #1805, 39.37007874015748143 ) ;
#828=CARTESIAN_POINT ( 'NONE',  ( 2.537500000000000533, 2.500000000000000444, 0.000000000000000000 ) ) ;
#830=EDGE_CURVE ( 'NONE', #3439, #3476, #4443, .T. ) ;
#833=AXIS2_PLACEMENT_3D ( 'NONE', #4893, #1664, #8023 ) ;
#838=B_SPLINE_CURVE_WITH_KNOTS ( 'NONE', 3,
 ( #5144, #4414, #6223, #5606 ),
 .UNSPECIFIED., .F., .F.,
 ( 4, 4 ),
 ( 3.040620560812911770E-12, 0.02101476597825354883 ),
 .UNSPECIFIED. ) ;
#839=AXIS2_PLACEMENT_3D ( 'NONE', #413, #5869, #7269 ) ;
#843=VERTEX_POINT ( 'NONE', #968 ) ;
#847=CARTESIAN_POINT ( 'NONE',  ( 1.500000000000000444, 5.414000000000000590, 0.000000000000000000 ) ) ;
#849=EDGE_CURVE ( 'NONE', #5226, #7577, #482, .T. ) ;
#850=AXIS2_PLACEMENT_3D ( 'NONE', #3466, #4604, #924 ) ;
#852=AXIS2_PLACEMENT_3D ( 'NONE', #6468, #1509, #1462 ) ;
#863=CARTESIAN_POINT ( 'NONE',  ( 1.312500000246545895, 7.352492874015749358, 3.316250000000001474 ) ) ;
#867=CIRCLE ( 'NONE', #8126, 2.619834094488189269 ) ;
#873=AXIS2_PLACEMENT_3D ( 'NONE', #5482, #5565, #5028 ) ;
#880=VECTOR ( 'NONE', #2867, 39.37007874015748143 ) ;
#881=ORIENTED_EDGE ( 'NONE', *, *, #6281, .F. ) ;
#882=EDGE_CURVE ( 'NONE', #8146, #691, #6317, .T. ) ;
#883=VECTOR ( 'NONE', #4336, 39.37007874015748143 ) ;
#884=DIRECTION ( 'NONE',  ( -0.000000000000000000, -0.000000000000000000, 1.000000000000000000 ) ) ;
#887=EDGE_CURVE ( 'NONE', #2392, #7545, #27, .T. ) ;
#891=DIRECTION ( 'NONE',  ( 1.000000000000000000, -0.000000000000000000, 0.000000000000000000 ) ) ;
#892=DIRECTION ( 'NONE',  ( -0.000000000000000000, -1.000000000000000000, 0.000000000000000000 ) ) ;
#894=ORIENTED_EDGE ( 'NONE', *, *, #2407, .F. ) ;
#895=FACE_OUTER_BOUND ( 'NONE', #1335, .T. ) ;
#897=DIRECTION ( 'NONE',  ( 0.000000000000000000, 0.000000000000000000, 1.000000000000000000 ) ) ;
#899=ADVANCED_FACE ( 'NONE', ( #3362, #3282 ), #2975, .T. ) ;
#900=ORIENTED_EDGE ( 'NONE', *, *, #5752, .F. ) ;
#904=ORIENTED_EDGE ( 'NONE', *, *, #3972, .F. ) ;
#906=CARTESIAN_POINT ( 'NONE',  ( 0.000000000000000000, 1.664000000000000368, 2.693920355039552791E-42 ) ) ;
#908=( CONVERSION_BASED_UNIT ( 'INCH', #7100 ) LENGTH_UNIT ( ) NAMED_UNIT ( #4284 ) );
#910=ORIENTED_EDGE ( 'NONE', *, *, #1941, .F. ) ;
#920=ORIENTED_EDGE ( 'NONE', *, *, #7725, .T. ) ;
#924=DIRECTION ( 'NONE',  ( -0.000000000000000000, 0.000000000000000000, -1.000000000000000000 ) ) ;
#939=DIRECTION ( 'NONE',  ( 0.000000000000000000, 0.000000000000000000, -1.000000000000000000 ) ) ;
#944=CARTESIAN_POINT ( 'NONE',  ( -1.138021853580373666, 3.294697891665690825, -5.108749999999999680 ) ) ;
#946=DIRECTION ( 'NONE',  ( -0.000000000000000000, 0.000000000000000000, 1.000000000000000000 ) ) ;
#957=DIRECTION ( 'NONE',  ( 1.000000000000000000, 0.000000000000000000, -0.000000000000000000 ) ) ;
#961=ORIENTED_EDGE ( 'NONE', *, *, #5735, .F. ) ;
#968=CARTESIAN_POINT ( 'NONE',  ( 1.500000000000000444, 5.414000000000000590, 2.750000000234376074 ) ) ;
#974=VECTOR ( 'NONE', #5005, 39.37007874015748143 ) ;
#978=DIRECTION ( 'NONE',  ( 0.000000000000000000, -1.000000000000000000, 0.000000000000000000 ) ) ;
#979=CARTESIAN_POINT ( 'NONE',  ( 2.750000000000002665, 8.589000000000000412, 3.161250000000001670 ) ) ;
#983=DIRECTION ( 'NONE',  ( 0.000000000000000000, 0.000000000000000000, -1.000000000000000000 ) ) ;
#986=DIRECTION ( 'NONE',  ( 0.000000000000000000, 0.000000000000000000, 1.000000000000000000 ) ) ;
#992=CIRCLE ( 'NONE', #1895, 1.624999999999999778 ) ;
#993=ADVANCED_FACE ( 'NONE', ( #4072 ), #4698, .F. ) ;
#994=CARTESIAN_POINT ( 'NONE',  ( -1.303938013533521678, 4.122802601861688565, -5.108750000000004121 ) ) ;
#996=CARTESIAN_POINT ( 'NONE',  ( -1.312500000000000444, 8.589000000000000412, 2.411250000000000782 ) ) ;
#1002=LINE ( 'NONE', #2878, #3964 ) ;
#1003=CARTESIAN_POINT ( 'NONE',  ( -1.500000000000000444, 5.414000000000000590, 0.000000000000000000 ) ) ;
#1011=DIRECTION ( 'NONE',  ( -0.000000000000000000, 1.000000000000000000, -0.000000000000000000 ) ) ;
#1013=ORIENTED_EDGE ( 'NONE', *, *, #3353, .F. ) ;
#1018=CARTESIAN_POINT ( 'NONE',  ( 1.312500000000000222, 7.339000000000000412, 3.239595687480216313 ) ) ;
#1022=CARTESIAN_POINT ( 'NONE',  ( -1.625000000000000222, 5.339000000000000412, 0.1250000000000000278 ) ) ;
#1026=DIRECTION ( 'NONE',  ( 1.000000000000000000, 0.000000000000000000, -0.000000000000000000 ) ) ;
#1029=ORIENTED_EDGE ( 'NONE', *, *, #3972, .T. ) ;
#1032=CARTESIAN_POINT ( 'NONE',  ( -1.282759086114038771, 4.228660313282746053, -5.108750000000003233 ) ) ;
#1033=DIRECTION ( 'NONE',  ( 1.000000000000000000, 0.000000000000000000, 0.000000000000000000 ) ) ;
#1034=CARTESIAN_POINT ( 'NONE',  ( -2.750000000000000444, 7.521783346456695440, 3.691250000000001030 ) ) ;
#1035=EDGE_CURVE ( 'NONE', #843, #4996, #7483, .T. ) ;
#1040=ADVANCED_FACE ( 'NONE', ( #4904 ), #1334, .T. ) ;
#1041=DIRECTION ( 'NONE',  ( 1.000000000000000000, 0.000000000000000000, -0.000000000000000000 ) ) ;
#1044=LINE ( 'NONE', #6814, #4354 ) ;
#1050=DIRECTION ( 'NONE',  ( 0.000000000000000000, 0.000000000000000000, -1.000000000000000000 ) ) ;
#1053=CARTESIAN_POINT ( 'NONE',  ( 3.296097360985625002, 1.750000000000000444, 0.5624999982029994516 ) ) ;
#1054=ORIENTED_EDGE ( 'NONE', *, *, #6520, .T. ) ;
#1057=CARTESIAN_POINT ( 'NONE',  ( 1.312500000000000222, 7.339000000000001300, 3.161250000000001670 ) ) ;
#1059=VERTEX_POINT ( 'NONE', #5597 ) ;
#1060=EDGE_LOOP ( 'NONE', ( #3167, #7736 ) ) ;
#1062=ORIENTED_EDGE ( 'NONE', *, *, #6498, .F. ) ;
#1069=PLANE ( 'NONE',  #4362 ) ;
#1077=EDGE_CURVE ( 'NONE', #674, #3226, #4552, .T. ) ;
#1079=CARTESIAN_POINT ( 'NONE',  ( 1.500000000000000444, 5.969165905511811587, 0.5414159055118110686 ) ) ;
#1084=ADVANCED_FACE ( 'NONE', ( #5554 ), #644, .F. ) ;
#1086=FACE_OUTER_BOUND ( 'NONE', #2054, .T. ) ;
#1087=CARTESIAN_POINT ( 'NONE',  ( 1.625000000000000222, 5.639000000000001123, -2.908930215307243383 ) ) ;
#1105=EDGE_CURVE ( 'NONE', #6766, #3004, #1148, .T. ) ;
#1106=ORIENTED_EDGE ( 'NONE', *, *, #3888, .T. ) ;
#1107=VECTOR ( 'NONE', #6433, 39.37007874015748143 ) ;
#1109=LINE ( 'NONE', #7357, #827 ) ;
#1113=VECTOR ( 'NONE', #2570, 39.37007874015748143 ) ;
#1114=DIRECTION ( 'NONE',  ( 0.000000000000000000, -0.000000000000000000, 1.000000000000000000 ) ) ;
#1125=CARTESIAN_POINT ( 'NONE',  ( -1.201750196850394081, 2.500000000000000444, -2.750000000000000444 ) ) ;
#1134=EDGE_LOOP ( 'NONE', ( #6358, #6595, #7126, #4769 ) ) ;
#1136=CARTESIAN_POINT ( 'NONE',  ( 0.000000000000000000, 0.000000000000000000, 0.1249999999999997641 ) ) ;
#1139=AXIS2_PLACEMENT_3D ( 'NONE', #3516, #278, #2773 ) ;
#1144=DIRECTION ( 'NONE',  ( 0.000000000000000000, -0.000000000000000000, 1.000000000000000000 ) ) ;
#1146=LINE ( 'NONE', #4789, #3871 ) ;
#1148=CIRCLE ( 'NONE', #5857, 1.624999999999999778 ) ;
#1151=ORIENTED_EDGE ( 'NONE', *, *, #1980, .F. ) ;
#1155=ORIENTED_EDGE ( 'NONE', *, *, #5576, .F. ) ;
#1156=EDGE_LOOP ( 'NONE', ( #7506, #4920, #4430, #1345 ) ) ;
#1165=CARTESIAN_POINT ( 'NONE',  ( -0.2598750118065171200, 2.345589018234187861, -3.059924881834113819 ) ) ;
#1172=CARTESIAN_POINT ( 'NONE',  ( -0.7052155605301347885, 5.414000000000000590, 0.5414159055118109576 ) ) ;
#1182=PRODUCT ( 'bench vise2-', 'bench vise2-', '', ( #498 ) ) ;
#1183=LINE ( 'NONE', #8004, #6979 ) ;
#1190=ORIENTED_EDGE ( 'NONE', *, *, #5387, .F. ) ;
#1192=EDGE_CURVE ( 'NONE', #3226, #6648, #127, .T. ) ;
#1193=EDGE_CURVE ( 'NONE', #540, #1793, #2196, .T. ) ;
#1194=ORIENTED_EDGE ( 'NONE', *, *, #249, .F. ) ;
#1201=CARTESIAN_POINT ( 'NONE',  ( -0.4484317010831837536, 2.386788549487817601, -3.019432426063724861 ) ) ;
#1202=CARTESIAN_POINT ( 'NONE',  ( -1.889618362131626726E-10, 5.414000000000000590, 2.750000000234376074 ) ) ;
#1207=CIRCLE ( 'NONE', #6454, 2.619834094488189269 ) ;
#1214=CARTESIAN_POINT ( 'NONE',  ( 0.7335700381840287720, 2.500000000317696536, -5.108750000000001457 ) ) ;
#1216=CARTESIAN_POINT ( 'NONE',  ( -3.343750000000001776, 2.500000000000000444, -2.750000000000000444 ) ) ;
#1221=ADVANCED_FACE ( 'NONE', ( #159 ), #6407, .T. ) ;
#1222=CARTESIAN_POINT ( 'NONE',  ( 1.624999999999999778, 3.950000000000000178, -2.749999999768383940 ) ) ;
#1232=ADVANCED_FACE ( 'NONE', ( #2102 ), #3412, .F. ) ;
#1234=EDGE_LOOP ( 'NONE', ( #894, #1547, #2489, #6495, #281, #4071, #6079, #4578 ) ) ;
#1236=CARTESIAN_POINT ( 'NONE',  ( 1.500000000000000444, 5.339000000000000412, 0.1249999999999998473 ) ) ;
#1237=CARTESIAN_POINT ( 'NONE',  ( 0.000000000000000000, 3.950000000000000178, -5.108750000000001457 ) ) ;
#1240=VERTEX_POINT ( 'NONE', #1490 ) ;
#1243=VECTOR ( 'NONE', #3425, 39.37007874015748143 ) ;
#1245=EDGE_CURVE ( 'NONE', #3378, #811, #6496, .T. ) ;
#1246=AXIS2_PLACEMENT_3D ( 'NONE', #1022, #4823, #2168 ) ;
#1248=CARTESIAN_POINT ( 'NONE',  ( 0.7631207292863003699, 2.881932780970207109, -5.108750000000001457 ) ) ;
#1254=ORIENTED_EDGE ( 'NONE', *, *, #4966, .F. ) ;
#1257=CARTESIAN_POINT ( 'NONE',  ( -1.312500000102930775, 4.908106857156239400, 3.316250000000001030 ) ) ;
#1259=DIRECTION ( 'NONE',  ( -1.000000000000000000, 0.000000000000000000, -0.000000000000000000 ) ) ;
#1269=CIRCLE ( 'NONE', #3865, 0.2625000000000008438 ) ;
#1270=VECTOR ( 'NONE', #7977, 39.37007874015748143 ) ;
#1274=ORIENTED_EDGE ( 'NONE', *, *, #1891, .F. ) ;
#1279=AXIS2_PLACEMENT_3D ( 'NONE', #2901, #5393, #2293 ) ;
#1281=ORIENTED_EDGE ( 'NONE', *, *, #7096, .F. ) ;
#1283=CYLINDRICAL_SURFACE ( 'NONE', #1759, 0.2625000000000008438 ) ;
#1285=ADVANCED_FACE ( 'NONE', ( #6584 ), #259, .T. ) ;
#1286=VERTEX_POINT ( 'NONE', #3449 ) ;
#1290=CARTESIAN_POINT ( 'NONE',  ( 1.310546128896300511, 4.033625775730570240, -5.108750000000004121 ) ) ;
#1292=ORIENTED_EDGE ( 'NONE', *, *, #1937, .T. ) ;
#1297=FACE_OUTER_BOUND ( 'NONE', #5302, .T. ) ;
#1299=ORIENTED_EDGE ( 'NONE', *, *, #4634, .T. ) ;
#1308=EDGE_LOOP ( 'NONE', ( #2995, #1054, #293, #7544 ) ) ;
#1313=EDGE_LOOP ( 'NONE', ( #30, #5281, #881, #8145 ) ) ;
#1320=CARTESIAN_POINT ( 'NONE',  ( -1.625000000000000222, 0.000000000000000000, 0.1249999999999997641 ) ) ;
#1323=ORIENTED_EDGE ( 'NONE', *, *, #7480, .T. ) ;
#1324=ORIENTED_EDGE ( 'NONE', *, *, #6787, .F. ) ;
#1326=CARTESIAN_POINT ( 'NONE',  ( 0.8990231340611340993, 4.907229921396190520, -5.108749999999997904 ) ) ;
#1329=LINE ( 'NONE', #1984, #346 ) ;
#1334=CYLINDRICAL_SURFACE ( 'NONE', #4802, 1.624999999999999778 ) ;
#1335=EDGE_LOOP ( 'NONE', ( #2095, #2588, #6189, #1323, #4194, #2430, #4467, #5777 ) ) ;
#1340=CARTESIAN_POINT ( 'NONE',  ( -1.624999999371729231, 2.076218724780642511, 2.750000000000000444 ) ) ;
#1343=DIRECTION ( 'NONE',  ( 0.000000000000000000, 0.000000000000000000, -1.000000000000000000 ) ) ;
#1344=CARTESIAN_POINT ( 'NONE',  ( -2.537500000000000533, 2.500000000000000444, -0.000000000000000000 ) ) ;
#1345=ORIENTED_EDGE ( 'NONE', *, *, #162, .F. ) ;
#1347=ORIENTED_EDGE ( 'NONE', *, *, #5584, .T. ) ;
#1350=DIRECTION ( 'NONE',  ( -0.000000000000000000, -1.000000000000000000, -0.000000000000000000 ) ) ;
#1357=DIRECTION ( 'NONE',  ( 0.000000000000000000, -1.000000000000000000, 0.000000000000000000 ) ) ;
#1358=CARTESIAN_POINT ( 'NONE',  ( -1.625000000000000222, 2.057992047244095346, -2.750000000000000444 ) ) ;
#1360=VECTOR ( 'NONE', #1435, 39.37007874015748143 ) ;
#1361=CARTESIAN_POINT ( 'NONE',  ( -1.625000000000000000, 3.950000000000000178, -2.750000000000000444 ) ) ;
#1364=VERTEX_POINT ( 'NONE', #2990 ) ;
#1367=CIRCLE ( 'NONE', #32, 3.000000000000001332 ) ;
#1369=CIRCLE ( 'NONE', #3841, 2.999999999836793663 ) ;
#1372=CARTESIAN_POINT ( 'NONE',  ( 0.7977802186893850900, 2.907566522260822239, -5.108750000000001457 ) ) ;
#1373=DIRECTION ( 'NONE',  ( 0.000000000000000000, 0.000000000000000000, -1.000000000000000000 ) ) ;
#1376=CARTESIAN_POINT ( 'NONE',  ( 0.000000000000000000, 3.950000000000000178, 3.316250000000001030 ) ) ;
#1379=VECTOR ( 'NONE', #2329, 39.37007874015748143 ) ;
#1382=FACE_OUTER_BOUND ( 'NONE', #6122, .T. ) ;
#1383=CARTESIAN_POINT ( 'NONE',  ( 0.000000000000000000, 5.151388682096968097, -2.750000000000000444 ) ) ;
#1402=ORIENTED_EDGE ( 'NONE', *, *, #6970, .T. ) ;
#1403=FACE_OUTER_BOUND ( 'NONE', #341, .T. ) ;
#1404=AXIS2_PLACEMENT_3D ( 'NONE', #5188, #2737, #7005 ) ;
#1405=CYLINDRICAL_SURFACE ( 'NONE', #2679, 1.624999999999999778 ) ;
#1407=AXIS2_PLACEMENT_3D ( 'NONE', #6609, #1754, #986 ) ;
#1409=ORIENTED_EDGE ( 'NONE', *, *, #6886, .F. ) ;
#1413=ORIENTED_EDGE ( 'NONE', *, *, #4346, .F. ) ;
#1415=CARTESIAN_POINT ( 'NONE',  ( 0.2965954892784562480, 2.670736509751080678, -5.108749999999998792 ) ) ;
#1417=CARTESIAN_POINT ( 'NONE',  ( 1.347488133127687560, 2.365290551318774082, 2.749999999536767437 ) ) ;
#1427=EDGE_CURVE ( 'NONE', #7586, #445, #1650, .T. ) ;
#1433=ADVANCED_FACE ( 'NONE', ( #4997 ), #8137, .F. ) ;
#1435=DIRECTION ( 'NONE',  ( 0.000000000000000000, 1.000000000000000000, 0.000000000000000000 ) ) ;
#1444=CARTESIAN_POINT ( 'NONE',  ( 2.750000000000000444, 8.589000000000000412, 3.161250000000001670 ) ) ;
#1448=ORIENTED_EDGE ( 'NONE', *, *, #2784, .T. ) ;
#1459=CARTESIAN_POINT ( 'NONE',  ( 3.343750000000001776, 0.000000000000000000, 0.000000000000000000 ) ) ;
#1462=DIRECTION ( 'NONE',  ( 0.000000000000000000, 0.000000000000000000, 1.000000000000000000 ) ) ;
#1478=CARTESIAN_POINT ( 'NONE',  ( -0.3427224271551993495, 2.680139432305034930, -5.108749999999998792 ) ) ;
#1481=CARTESIAN_POINT ( 'NONE',  ( -2.750000000000000444, 7.339000000000003077, 2.411250000000000338 ) ) ;
#1483=CARTESIAN_POINT ( 'NONE',  ( 0.7052155605301347885, 5.414000000000000590, 0.1249999999999999029 ) ) ;
#1484=ORIENTED_EDGE ( 'NONE', *, *, #2339, .F. ) ;
#1490=CARTESIAN_POINT ( 'NONE',  ( -3.343750000000002220, 1.749999999935557327, 0.5625000000000003331 ) ) ;
#1493=AXIS2_PLACEMENT_3D ( 'NONE', #1652, #5285, #4754 ) ;
#1501=VECTOR ( 'NONE', #692, 39.37007874015748143 ) ;
#1504=VECTOR ( 'NONE', #133, 39.37007874015748143 ) ;
#1505=VECTOR ( 'NONE', #627, 39.37007874015748143 ) ;
#1507=VERTEX_POINT ( 'NONE', #3199 ) ;
#1509=DIRECTION ( 'NONE',  ( -1.000000000000000000, 0.000000000000000000, 0.000000000000000000 ) ) ;
#1525=AXIS2_PLACEMENT_3D ( 'NONE', #4566, #3863, #3341 ) ;
#1526=DIRECTION ( 'NONE',  ( -0.000000000000000000, 1.000000000000000000, -0.000000000000000000 ) ) ;
#1528=CARTESIAN_POINT ( 'NONE',  ( -1.201750196850394081, 2.500000000000000444, -2.750000000000000444 ) ) ;
#1534=DIRECTION ( 'NONE',  ( 0.000000000000000000, -0.000000000000000000, 1.000000000000000000 ) ) ;
#1538=EDGE_CURVE ( 'NONE', #4491, #1578, #5591, .T. ) ;
#1540=PLANE ( 'NONE',  #3451 ) ;
#1542=ORIENTED_EDGE ( 'NONE', *, *, #3875, .F. ) ;
#1543=VECTOR ( 'NONE', #5875, 39.37007874015748143 ) ;
#1544=CARTESIAN_POINT ( 'NONE',  ( 1.274606805570081214, 2.434036455782362829, -2.749999999536767437 ) ) ;
#1547=ORIENTED_EDGE ( 'NONE', *, *, #4549, .F. ) ;
#1549=LINE ( 'NONE', #4030, #6499 ) ;
#1553=FACE_OUTER_BOUND ( 'NONE', #6757, .T. ) ;
#1556=DIRECTION ( 'NONE',  ( 0.000000000000000000, -0.000000000000000000, -1.000000000000000000 ) ) ;
#1558=ORIENTED_EDGE ( 'NONE', *, *, #1077, .T. ) ;
#1563=CARTESIAN_POINT ( 'NONE',  ( 0.001186118861278498285, 5.262499470843738258, -5.108750000000001457 ) ) ;
#1564=CARTESIAN_POINT ( 'NONE',  ( -1.136188160962484872, 4.607419020399388110, -5.108750000000003233 ) ) ;
#1565=CARTESIAN_POINT ( 'NONE',  ( 1.249999999999999556, 3.950000000000000178, -4.308749999765625560 ) ) ;
#1570=DIRECTION ( 'NONE',  ( 0.000000000000000000, 1.000000000000000000, 0.000000000000000000 ) ) ;
#1572=ADVANCED_FACE ( 'NONE', ( #1814 ), #575, .F. ) ;
#1578=VERTEX_POINT ( 'NONE', #8181 ) ;
#1580=LINE ( 'NONE', #4060, #2530 ) ;
#1582=CARTESIAN_POINT ( 'NONE',  ( 1.625000000000000222, 5.339000000000000412, -2.750000000000000444 ) ) ;
#1584=EDGE_CURVE ( 'NONE', #8024, #3627, #3237, .T. ) ;
#1585=ADVANCED_FACE ( 'NONE', ( #1403 ), #6359, .F. ) ;
#1586=CARTESIAN_POINT ( 'NONE',  ( 0.1311681248375602682, 2.329016406037186737, -3.076246856427637510 ) ) ;
#1588=ORIENTED_EDGE ( 'NONE', *, *, #735, .F. ) ;
#1591=CARTESIAN_POINT ( 'NONE',  ( -0.7052155605301346775, 5.414000000000000590, 0.000000000000000000 ) ) ;
#1596=ORIENTED_EDGE ( 'NONE', *, *, #228, .F. ) ;
#1598=CARTESIAN_POINT ( 'NONE',  ( 1.625000000000000222, 5.113999999999999879, 2.750000000000000444 ) ) ;
#1599=LINE ( 'NONE', #6607, #1379 ) ;
#1600=LINE ( 'NONE', #4579, #3335 ) ;
#1602=DIRECTION ( 'NONE',  ( -0.000000000000000000, 1.000000000000000000, -0.000000000000000000 ) ) ;
#1604=ORIENTED_EDGE ( 'NONE', *, *, #1192, .T. ) ;
#1605=CARTESIAN_POINT ( 'NONE',  ( -0.7665824524342863544, 2.883775449096970256, -5.108750000000003233 ) ) ;
#1606=EDGE_CURVE ( 'NONE', #5196, #8146, #7404, .T. ) ;
#1607=CARTESIAN_POINT ( 'NONE',  ( 0.08076397176416273693, 2.326924981622356281, 3.078310609319442115 ) ) ;
#1611=ORIENTED_EDGE ( 'NONE', *, *, #5286, .F. ) ;
#1617=ORIENTED_EDGE ( 'NONE', *, *, #2536, .F. ) ;
#1618=VECTOR ( 'NONE', #5923, 39.37007874015748143 ) ;
#1621=CARTESIAN_POINT ( 'NONE',  ( -3.343750000000001776, 1.750000000000000444, -0.5625000000000003331 ) ) ;
#1628=DIRECTION ( 'NONE',  ( 0.000000000000000000, 1.000000000000000000, 0.000000000000000000 ) ) ;
#1632=VERTEX_POINT ( 'NONE', #6842 ) ;
#1638=CARTESIAN_POINT ( 'NONE',  ( -0.7335700375402988138, 2.499999999992026378, 2.908930215739981229 ) ) ;
#1639=VECTOR ( 'NONE', #4243, 39.37007874015748143 ) ;
#1641=CARTESIAN_POINT ( 'NONE',  ( -1.624999999560674535, 2.217843349570411515, 2.674602988970680606 ) ) ;
#1642=EDGE_CURVE ( 'NONE', #3433, #5914, #5864, .T. ) ;
#1643=FACE_OUTER_BOUND ( 'NONE', #7950, .T. ) ;
#1644=AXIS2_PLACEMENT_3D ( 'NONE', #399, #2892, #1556 ) ;
#1646=CARTESIAN_POINT ( 'NONE',  ( -1.624999999999998446, 5.151388682096968097, 2.750000000000000444 ) ) ;
#1649=ORIENTED_EDGE ( 'NONE', *, *, #6889, .T. ) ;
#1650=LINE ( 'NONE', #4133, #1804 ) ;
#1651=AXIS2_PLACEMENT_3D ( 'NONE', #7721, #7636, #6336 ) ;
#1652=CARTESIAN_POINT ( 'NONE',  ( -1.312500000000000444, 4.908106850393701315, 3.316250000000001474 ) ) ;
#1656=CARTESIAN_POINT ( 'NONE',  ( 1.625000000000000222, 5.339000000000000412, -2.750000000000000444 ) ) ;
#1660=EDGE_CURVE ( 'NONE', #5594, #7750, #5230, .T. ) ;
#1663=CARTESIAN_POINT ( 'NONE',  ( 0.5365888410826438193, 2.415836454015215295, -2.990976592206287421 ) ) ;
#1664=DIRECTION ( 'NONE',  ( -0.000000000000000000, 1.000000000000000000, -0.000000000000000000 ) ) ;
#1667=AXIS2_PLACEMENT_3D ( 'NONE', #5666, #489, #6290 ) ;
#1672=EDGE_LOOP ( 'NONE', ( #7779, #6478, #6427, #4554 ) ) ;
#1677=ORIENTED_EDGE ( 'NONE', *, *, #5516, .F. ) ;
#1682=ORIENTED_EDGE ( 'NONE', *, *, #4549, .T. ) ;
#1686=CARTESIAN_POINT ( 'NONE',  ( -0.8148948558711907042, 4.979111548578501356, -5.108750000000004121 ) ) ;
#1691=ORIENTED_EDGE ( 'NONE', *, *, #3137, .T. ) ;
#1694=EDGE_CURVE ( 'NONE', #8024, #6387, #7652, .T. ) ;
#1695=FACE_OUTER_BOUND ( 'NONE', #439, .T. ) ;
#1696=CARTESIAN_POINT ( 'NONE',  ( 0.000000000000000000, 3.950000000000000178, 3.691250000234376660 ) ) ;
#1698=CARTESIAN_POINT ( 'NONE',  ( 1.625000000000000222, 2.499999999434268982, 2.521780125537467665 ) ) ;
#1699=VERTEX_POINT ( 'NONE', #3401 ) ;
#1702=LINE ( 'NONE', #1582, #6331 ) ;
#1703=CARTESIAN_POINT ( 'NONE',  ( 1.500000000000000444, 5.414000000000000590, 0.1249999999999999029 ) ) ;
#1705=CARTESIAN_POINT ( 'NONE',  ( 1.318571496062992399, 2.714076811023622415, -7.382249173228347949 ) ) ;
#1710=LINE ( 'NONE', #2454, #5971 ) ;
#1721=VERTEX_POINT ( 'NONE', #6394 ) ;
#1734=ORIENTED_EDGE ( 'NONE', *, *, #3380, .F. ) ;
#1735=DIRECTION ( 'NONE',  ( -1.000000000000000000, -0.000000000000000000, -0.000000000000000000 ) ) ;
#1736=ORIENTED_EDGE ( 'NONE', *, *, #4476, .F. ) ;
#1737=CARTESIAN_POINT ( 'NONE',  ( -0.06606835743134251149, 2.325000000000000622, -3.080208333333334547 ) ) ;
#1740=ADVANCED_FACE ( 'NONE', ( #3684 ), #8129, .T. ) ;
#1741=LINE ( 'NONE', #3632, #7125 ) ;
#1746=CIRCLE ( 'NONE', #7396, 2.841000000000000636 ) ;
#1754=DIRECTION ( 'NONE',  ( -0.000000000000000000, 1.000000000000000000, -0.000000000000000000 ) ) ;
#1755=EDGE_LOOP ( 'NONE', ( #4157, #7008, #1324, #6449 ) ) ;
#1759=AXIS2_PLACEMENT_3D ( 'NONE', #6155, #7414, #6774 ) ;
#1767=CIRCLE ( 'NONE', #6862, 1.624999999999999778 ) ;
#1777=CARTESIAN_POINT ( 'NONE',  ( -0.7335700376807066103, 2.500000000063059780, 2.750000000000000888 ) ) ;
#1783=ORIENTED_EDGE ( 'NONE', *, *, #177, .T. ) ;
#1789=ORIENTED_EDGE ( 'NONE', *, *, #2647, .F. ) ;
#1793=VERTEX_POINT ( 'NONE', #2502 ) ;
#1795=CONICAL_SURFACE ( 'NONE', #1139, 3.343750000040417447, 0.4297622790966887374 ) ;
#1798=EDGE_CURVE ( 'NONE', #6749, #4596, #1269, .T. ) ;
#1801=FACE_OUTER_BOUND ( 'NONE', #7418, .T. ) ;
#1803=CIRCLE ( 'NONE', #3317, 0.2625000000000008438 ) ;
#1804=VECTOR ( 'NONE', #1041, 39.37007874015748143 ) ;
#1805=DIRECTION ( 'NONE',  ( 0.000000000000000000, 1.000000000000000000, -0.000000000000000000 ) ) ;
#1807=DIRECTION ( 'NONE',  ( 0.000000000000000000, 0.000000000000000000, 1.000000000000000000 ) ) ;
#1811=CARTESIAN_POINT ( 'NONE',  ( 0.000000000000000000, 5.414000000000000590, 0.5414159055118109576 ) ) ;
#1814=FACE_OUTER_BOUND ( 'NONE', #3693, .T. ) ;
#1816=CARTESIAN_POINT ( 'NONE',  ( -2.946793808642157231, 2.500000000130568889, -0.5624999991015005030 ) ) ;
#1821=EDGE_CURVE ( 'NONE', #2706, #5748, #5847, .T. ) ;
#1822=CARTESIAN_POINT ( 'NONE',  ( 3.296097360936645959, 1.749999999910763826, -0.5625000000000002220 ) ) ;
#1823=CARTESIAN_POINT ( 'NONE',  ( 0.03453472440944883176, 5.297609015748031780, -5.034819094488189428 ) ) ;
#1828=FACE_OUTER_BOUND ( 'NONE', #3259, .T. ) ;
#1830=CARTESIAN_POINT ( 'NONE',  ( 0.000000000000000000, 3.950000000000000178, -5.108750000000001457 ) ) ;
#1842=CARTESIAN_POINT ( 'NONE',  ( -3.296097360993826886, 1.750000000000000444, -0.5624999982030005619 ) ) ;
#1844=VERTEX_POINT ( 'NONE', #4415 ) ;
#1848=FACE_OUTER_BOUND ( 'NONE', #1936, .T. ) ;
#1849=DIRECTION ( 'NONE',  ( -0.000000000000000000, -0.000000000000000000, 1.000000000000000000 ) ) ;
#1856=DIRECTION ( 'NONE',  ( 0.000000000000000000, -0.000000000000000000, 1.000000000000000000 ) ) ;
#1860=DIRECTION ( 'NONE',  ( -1.000000000000000000, 0.000000000000000000, 0.000000000000000000 ) ) ;
#1865=CARTESIAN_POINT ( 'NONE',  ( 1.625000000000000222, 2.359134605886186620, 2.598586947110950174 ) ) ;
#1866=AXIS2_PLACEMENT_3D ( 'NONE', #2543, #5030, #5687 ) ;
#1874=AXIS2_PLACEMENT_3D ( 'NONE', #1344, #3835, #1807 ) ;
#1875=AXIS2_PLACEMENT_3D ( 'NONE', #6262, #2535, #4486 ) ;
#1880=ORIENTED_EDGE ( 'NONE', *, *, #6956, .T. ) ;
#1881=CARTESIAN_POINT ( 'NONE',  ( -1.312500000000000444, 5.969165905511811587, 0.5414159055118118458 ) ) ;
#1887=DIRECTION ( 'NONE',  ( 0.000000000000000000, -1.000000000000000000, 0.000000000000000000 ) ) ;
#1888=AXIS2_PLACEMENT_3D ( 'NONE', #4083, #6619, #331 ) ;
#1889=AXIS2_PLACEMENT_3D ( 'NONE', #6156, #2308, #7416 ) ;
#1891=EDGE_CURVE ( 'NONE', #6458, #1952, #772, .T. ) ;
#1894=ORIENTED_EDGE ( 'NONE', *, *, #1105, .T. ) ;
#1895=AXIS2_PLACEMENT_3D ( 'NONE', #5796, #5918, #5295 ) ;
#1905=VECTOR ( 'NONE', #4067, 39.37007874015748143 ) ;
#1907=CARTESIAN_POINT ( 'NONE',  ( -2.749999999999998668, 8.589000000000000412, 2.411250000000000782 ) ) ;
#1909=ORIENTED_EDGE ( 'NONE', *, *, #2354, .F. ) ;
#1912=DIRECTION ( 'NONE',  ( 1.000000000000000000, 0.000000000000000000, 0.000000000000000000 ) ) ;
#1915=DIRECTION ( 'NONE',  ( 0.000000000000000000, 0.000000000000000000, -1.000000000000000000 ) ) ;
#1917=VECTOR ( 'NONE', #8001, 39.37007874015748143 ) ;
#1919=EDGE_CURVE ( 'NONE', #7750, #8146, #4401, .T. ) ;
#1923=VERTEX_POINT ( 'NONE', #1995 ) ;
#1930=EDGE_CURVE ( 'NONE', #5914, #1364, #7027, .T. ) ;
#1936=EDGE_LOOP ( 'NONE', ( #106, #5927, #3698, #4586 ) ) ;
#1937=EDGE_CURVE ( 'NONE', #1923, #4674, #6366, .T. ) ;
#1941=EDGE_CURVE ( 'NONE', #7519, #811, #5444, .T. ) ;
#1943=CARTESIAN_POINT ( 'NONE',  ( 1.303938020448307977, 3.777197438547405639, -5.108750000000002345 ) ) ;
#1945=VERTEX_POINT ( 'NONE', #2579 ) ;
#1949=DIRECTION ( 'NONE',  ( 0.000000000000000000, 0.000000000000000000, -1.000000000000000000 ) ) ;
#1950=CARTESIAN_POINT ( 'NONE',  ( 1.312500000000000444, 4.908106850393701315, 2.750000000234376074 ) ) ;
#1951=CARTESIAN_POINT ( 'NONE',  ( 0.000000000000000000, 3.950000000000000178, 2.749999998413802604 ) ) ;
#1952=VERTEX_POINT ( 'NONE', #104 ) ;
#1955=EDGE_CURVE ( 'NONE', #4397, #4996, #5145, .T. ) ;
#1957=CARTESIAN_POINT ( 'NONE',  ( 2.946793809113656959, 2.499999999120089189, 0.5624999991014997258 ) ) ;
#1959=DIRECTION ( 'NONE',  ( -0.000000000000000000, 1.000000000000000000, -0.000000000000000000 ) ) ;
#1964=CARTESIAN_POINT ( 'NONE',  ( -2.750000000000000444, 7.531471846334603981, 3.702890677416158294 ) ) ;
#1969=CARTESIAN_POINT ( 'NONE',  ( 0.000000000000000000, 1.750000000000000444, 2.693920355039552791E-42 ) ) ;
#1972=CARTESIAN_POINT ( 'NONE',  ( 2.537500000000000533, 2.500000000000000444, 0.000000000000000000 ) ) ;
#1975=DIRECTION ( 'NONE',  ( 1.000000000000000000, 0.000000000000000000, 0.000000000000000000 ) ) ;
#1976=ORIENTED_EDGE ( 'NONE', *, *, #1660, .T. ) ;
#1977=EDGE_CURVE ( 'NONE', #1952, #266, #867, .T. ) ;
#1978=ORIENTED_EDGE ( 'NONE', *, *, #113, .T. ) ;
#1980=EDGE_CURVE ( 'NONE', #1286, #8146, #7211, .T. ) ;
#1982=CARTESIAN_POINT ( 'NONE',  ( 0.4616491041369191750, 2.720615487789157072, -5.108750000000005009 ) ) ;
#1984=CARTESIAN_POINT ( 'NONE',  ( -1.312500000205861328, 4.908106857015235747, -5.108750000000001457 ) ) ;
#1987=FACE_OUTER_BOUND ( 'NONE', #2336, .T. ) ;
#1988=EDGE_LOOP ( 'NONE', ( #6196, #2281, #7287, #1542 ) ) ;
#1995=CARTESIAN_POINT ( 'NONE',  ( -1.249999999999999556, 3.950000000000000178, -4.308749999765625560 ) ) ;
#1998=VERTEX_POINT ( 'NONE', #3477 ) ;
#2003=CARTESIAN_POINT ( 'NONE',  ( 2.750000000000003109, 7.339000000000003077, 2.411250000000000782 ) ) ;
#2005=DIRECTION ( 'NONE',  ( -1.000000000000000000, -0.000000000000000000, -0.000000000000000000 ) ) ;
#2008=CARTESIAN_POINT ( 'NONE',  ( 1.625000000000000222, 2.500000000000000000, 2.750000000000000444 ) ) ;
#2016=CIRCLE ( 'NONE', #839, 0.2625000000000008438 ) ;
#2020=CARTESIAN_POINT ( 'NONE',  ( 0.1740164558986418974, 5.251634619451294839, -5.108750000000001457 ) ) ;
#2024=CARTESIAN_POINT ( 'NONE',  ( 1.557862129563219122, 2.150738730688390721, 2.749999999536767437 ) ) ;
#2026=ADVANCED_FACE ( 'NONE', ( #895 ), #7306, .T. ) ;
#2028=B_SPLINE_CURVE_WITH_KNOTS ( 'NONE', 3,
 ( #5463, #4854, #7379, #6748 ),
 .UNSPECIFIED., .F., .F.,
 ( 4, 4 ),
 ( 0.000000000000000000, 0.01222568466273604368 ),
 .UNSPECIFIED. ) ;
#2034=DIRECTION ( 'NONE',  ( -0.000000000000000000, -0.000000000000000000, 1.000000000000000000 ) ) ;
#2037=CIRCLE ( 'NONE', #1525, 1.624999999999999778 ) ;
#2045=CARTESIAN_POINT ( 'NONE',  ( 1.312500000000000444, 5.969165905511811587, 3.161250000000001670 ) ) ;
#2047=ORIENTED_EDGE ( 'NONE', *, *, #5849, .F. ) ;
#2051=DIRECTION ( 'NONE',  ( 0.000000000000000000, -0.000000000000000000, 1.000000000000000000 ) ) ;
#2054=EDGE_LOOP ( 'NONE', ( #2935, #5695 ) ) ;
#2055=AXIS2_PLACEMENT_3D ( 'NONE', #1598, #4034, #2891 ) ;
#2057=ADVANCED_FACE ( 'NONE', ( #2934 ), #1795, .T. ) ;
#2059=CARTESIAN_POINT ( 'NONE',  ( -2.750000000000000444, 8.589000000000000412, 3.161250000000001670 ) ) ;
#2064=VERTEX_POINT ( 'NONE', #2208 ) ;
#2067=CARTESIAN_POINT ( 'NONE',  ( 0.5808953724622998305, 2.769908242203201976, -5.108750000000004121 ) ) ;
#2069=ORIENTED_EDGE ( 'NONE', *, *, #2396, .T. ) ;
#2082=ADVANCED_FACE ( 'NONE', ( #4654 ), #7170, .F. ) ;
#2085=ORIENTED_EDGE ( 'NONE', *, *, #7938, .F. ) ;
#2090=ORIENTED_EDGE ( 'NONE', *, *, #7157, .T. ) ;
#2095=ORIENTED_EDGE ( 'NONE', *, *, #4977, .T. ) ;
#2097=CARTESIAN_POINT ( 'NONE',  ( -1.500000000000000444, 5.339000000000000412, 0.1249999999999999029 ) ) ;
#2101=ORIENTED_EDGE ( 'NONE', *, *, #7167, .T. ) ;
#2102=FACE_OUTER_BOUND ( 'NONE', #1156, .T. ) ;
#2111=CARTESIAN_POINT ( 'NONE',  ( -1.249999999999999556, 3.950000000000000178, 3.691250000234376660 ) ) ;
#2118=CARTESIAN_POINT ( 'NONE',  ( -2.946793808531571468, 2.500000000000000000, 0.5625000000000002220 ) ) ;
#2121=CARTESIAN_POINT ( 'NONE',  ( 0.000000000000000000, 1.750000000000000666, 0.000000000000000000 ) ) ;
#2130=CARTESIAN_POINT ( 'NONE',  ( -1.205291321983570585, 3.430008700001376365, -5.108749999999999680 ) ) ;
#2131=DIRECTION ( 'NONE',  ( 0.000000000000000000, 0.000000000000000000, -1.000000000000000000 ) ) ;
#2133=ORIENTED_EDGE ( 'NONE', *, *, #3380, .T. ) ;
#2136=AXIS2_PLACEMENT_3D ( 'NONE', #906, #6487, #5197 ) ;
#2155=ORIENTED_EDGE ( 'NONE', *, *, #5683, .F. ) ;
#2161=CIRCLE ( 'NONE', #3077, 1.249999999999999556 ) ;
#2168=DIRECTION ( 'NONE',  ( 0.000000000000000000, -0.000000000000000000, 1.000000000000000000 ) ) ;
#2173=B_SPLINE_CURVE_WITH_KNOTS ( 'NONE', 3,
 ( #1563, #3440, #5475, #2416, #2376, #7393, #4245, #3646, #4292, #5738, #2786, #4791, #1686, #6686, #5728, #2178, #329, #4010, #4667, #1564, #4590, #3958, #251, #6618, #2747, #4044, #7913, #1032, #994, #6535, #2250, #4742, #5823, #6578, #4705, #3489, #4081, #7097, #2130, #7181, #288, #2712, #944, #2828, #3442, #5943, #5902, #7222, #5318, #1605, #2785, #5273, #5990, #7782, #7138, #1478, #2868, #7874, #367, #2218, #7828 ),
 .UNSPECIFIED., .F., .F.,
 ( 4, 2, 2, 2, 2, 2, 2, 2, 2, 2, 2, 1, 2, 2, 2, 2, 2, 2, 2, 2, 2, 2, 2, 2, 2, 2, 2, 2, 2, 2, 4 ),
 ( 0.000000000000000000, 0.006512929480687936271, 0.009769394221031912212, 0.01302585896137588989, 0.01953878844206384177, 0.02116702081223586010, 0.02279525318240787496, 0.02605171792275184917, 0.03256464740343981840, 0.03419287977361179509, 0.03582111214378377179, 0.03907757688412773212, 0.04233404162447169244, 0.04396227399464366220, 0.04559050636481563890, 0.05210343584550344159, 0.05535990058584736723, 0.05698813295601932311, 0.05861636532619128592, 0.06512929480687901229, 0.06675752717705098205, 0.06838575954722293793, 0.07164222428756686356, 0.07815515376825467320, 0.08141161850859858495, 0.08466808324894249671, 0.08792454798928640847, 0.09118101272963030635, 0.09769394221031812986, 0.1009504069506620277, 0.1042068716910059117 ),
 .UNSPECIFIED. ) ;
#2175=ORIENTED_EDGE ( 'NONE', *, *, #5942, .T. ) ;
#2177=B_SPLINE_CURVE_WITH_KNOTS ( 'NONE', 3,
 ( #5680, #5067, #4369, #1957 ),
 .UNSPECIFIED., .F., .F.,
 ( 4, 4 ),
 ( 0.000000000000000000, 0.02101476594778851903 ),
 .UNSPECIFIED. ) ;
#2178=CARTESIAN_POINT ( 'NONE',  ( -0.9878476136873203250, 4.818414295186383534, -5.108749999999999680 ) ) ;
#2179=CARTESIAN_POINT ( 'NONE',  ( -0.3232363751884362868, 2.357145915514489598, 3.048554855073091652 ) ) ;
#2183=VERTEX_POINT ( 'NONE', #6171 ) ;
#2184=AXIS2_PLACEMENT_3D ( 'NONE', #3651, #8043, #7450 ) ;
#2189=AXIS2_PLACEMENT_3D ( 'NONE', #4860, #3597, #518 ) ;
#2196=CIRCLE ( 'NONE', #1667, 3.000000000000000888 ) ;
#2202=PLANE ( 'NONE',  #852 ) ;
#2206=PRODUCT_DEFINITION_FORMATION_WITH_SPECIFIED_SOURCE ( 'ANY', '', #1182, .NOT_KNOWN. ) ;
#2208=CARTESIAN_POINT ( 'NONE',  ( -1.249999999999999556, 3.950000000000000178, 3.691250000234376660 ) ) ;
#2209=VERTEX_POINT ( 'NONE', #8070 ) ;
#2218=CARTESIAN_POINT ( 'NONE',  ( -0.04453717661363842256, 2.637539714682124892, -5.108750000000001457 ) ) ;
#2219=CARTESIAN_POINT ( 'NONE',  ( 0.1625041179141621384, 2.332820669151155712, 3.072499754721300214 ) ) ;
#2220=DIRECTION ( 'NONE',  ( -0.000000000000000000, -0.000000000000000000, -1.000000000000000000 ) ) ;
#2223=VERTEX_POINT ( 'NONE', #2370 ) ;
#2225=PLANE ( 'NONE',  #1493 ) ;
#2231=ADVANCED_FACE ( 'NONE', ( #1828 ), #3675, .T. ) ;
#2239=CARTESIAN_POINT ( 'NONE',  ( 0.7052155605301347885, 5.414000000000000590, 0.5414159055118110686 ) ) ;
#2246=DIRECTION ( 'NONE',  ( -0.000000000000000000, 1.000000000000000000, 0.000000000000000000 ) ) ;
#2248=ORIENTED_EDGE ( 'NONE', *, *, #2807, .F. ) ;
#2249=DIRECTION ( 'NONE',  ( -1.000000000000000000, 0.000000000000000000, -0.000000000000000000 ) ) ;
#2250=CARTESIAN_POINT ( 'NONE',  ( -1.312565957648427428, 3.909279572067391850, -5.108750000000001457 ) ) ;
#2251=CARTESIAN_POINT ( 'NONE',  ( -0.6796865136544424368, 2.472739766459443267, 2.935403920510917253 ) ) ;
#2252=LINE ( 'NONE', #1646, #4232 ) ;
#2253=CARTESIAN_POINT ( 'NONE',  ( -1.312500000000001110, 7.339000000000003077, 3.239595687665816737 ) ) ;
#2260=DIRECTION ( 'NONE',  ( 0.000000000000000000, 0.000000000000000000, 1.000000000000000000 ) ) ;
#2267=DIRECTION ( 'NONE',  ( -0.000000000000000000, -1.000000000000000000, 0.000000000000000000 ) ) ;
#2268=CARTESIAN_POINT ( 'NONE',  ( 0.000000000000000000, 2.325000000000000622, -3.080208333333334103 ) ) ;
#2271=VERTEX_POINT ( 'NONE', #1257 ) ;
#2278=CIRCLE ( 'NONE', #8099, 0.2625000000000008438 ) ;
#2279=ORIENTED_EDGE ( 'NONE', *, *, #8114, .T. ) ;
#2280=ADVANCED_FACE ( 'NONE', ( #6712 ), #7343, .F. ) ;
#2281=ORIENTED_EDGE ( 'NONE', *, *, #216, .T. ) ;
#2284=VERTEX_POINT ( 'NONE', #676 ) ;
#2286=ADVANCED_FACE ( 'NONE', ( #3257 ), #5719, .T. ) ;
#2288=VECTOR ( 'NONE', #4955, 39.37007874015748143 ) ;
#2291=ORIENTED_EDGE ( 'NONE', *, *, #2446, .F. ) ;
#2293=DIRECTION ( 'NONE',  ( 1.000000000000000000, 0.000000000000000000, 0.000000000000000000 ) ) ;
#2302=VERTEX_POINT ( 'NONE', #4523 ) ;
#2306=CARTESIAN_POINT ( 'NONE',  ( 1.625000000000000222, 5.113999999999999879, -2.749999999536767437 ) ) ;
#2308=DIRECTION ( 'NONE',  ( -0.000000000000000000, 1.000000000000000000, 0.000000000000000000 ) ) ;
#2311=ORIENTED_EDGE ( 'NONE', *, *, #7444, .T. ) ;
#2314=VECTOR ( 'NONE', #2643, 39.37007874015748143 ) ;
#2318=DIRECTION ( 'NONE',  ( -0.000000000000000000, 0.000000000000000000, 1.000000000000000000 ) ) ;
#2319=CARTESIAN_POINT ( 'NONE',  ( 0.000000000000000000, 2.500000000356088936, 0.000000000000000000 ) ) ;
#2320=DIRECTION ( 'NONE',  ( -0.000000000000000000, -0.000000000000000000, 1.000000000000000000 ) ) ;
#2321=AXIS2_PLACEMENT_3D ( 'NONE', #3266, #7687, #1915 ) ;
#2328=DIRECTION ( 'NONE',  ( -0.000000000000000000, -0.000000000000000000, 1.000000000000000000 ) ) ;
#2329=DIRECTION ( 'NONE',  ( -0.000000000000000000, 0.000000000000000000, -1.000000000000000000 ) ) ;
#2336=EDGE_LOOP ( 'NONE', ( #1617, #4325, #6298, #5291 ) ) ;
#2339=EDGE_CURVE ( 'NONE', #6387, #4731, #4809, .T. ) ;
#2342=CARTESIAN_POINT ( 'NONE',  ( 0.7335700383901263555, 2.500000000202698303, 2.908930215426092758 ) ) ;
#2344=CARTESIAN_POINT ( 'NONE',  ( -1.500000000000000444, 5.414000000000000590, 2.749999998413802160 ) ) ;
#2354=EDGE_CURVE ( 'NONE', #2284, #2355, #1146, .T. ) ;
#2355=VERTEX_POINT ( 'NONE', #7912 ) ;
#2358=LINE ( 'NONE', #7241, #1360 ) ;
#2362=VERTEX_POINT ( 'NONE', #3018 ) ;
#2367=EDGE_CURVE ( 'NONE', #5914, #3226, #6144, .T. ) ;
#2370=CARTESIAN_POINT ( 'NONE',  ( -3.343750000000002220, 1.750000000000000444, -0.5624999991015005030 ) ) ;
#2373=ORIENTED_EDGE ( 'NONE', *, *, #2768, .T. ) ;
#2376=CARTESIAN_POINT ( 'NONE',  ( -0.3381868542694876911, 5.218913450356295058, -5.108750000000003233 ) ) ;
#2383=EDGE_CURVE ( 'NONE', #6055, #2284, #6023, .T. ) ;
#2384=FACE_OUTER_BOUND ( 'NONE', #7432, .T. ) ;
#2389=ORIENTED_EDGE ( 'NONE', *, *, #548, .T. ) ;
#2390=DIRECTION ( 'NONE',  ( -0.000000000000000000, 1.000000000000000000, -0.000000000000000000 ) ) ;
#2392=VERTEX_POINT ( 'NONE', #6616 ) ;
#2394=EDGE_LOOP ( 'NONE', ( #3021, #3642, #3652, #8118, #4951, #1106 ) ) ;
#2396=EDGE_CURVE ( 'NONE', #2706, #6912, #2944, .T. ) ;
#2398=CARTESIAN_POINT ( 'NONE',  ( -1.161591181102362702, 3.052477677165355008, -4.271824881889764391 ) ) ;
#2403=LINE ( 'NONE', #6091, #4264 ) ;
#2405=CIRCLE ( 'NONE', #7801, 3.343750000000001332 ) ;
#2407=EDGE_CURVE ( 'NONE', #3267, #4783, #3245, .T. ) ;
#2408=ORIENTED_EDGE ( 'NONE', *, *, #849, .F. ) ;
#2415=DIRECTION ( 'NONE',  ( 0.000000000000000000, -0.000000000000000000, 1.000000000000000000 ) ) ;
#2416=CARTESIAN_POINT ( 'NONE',  ( -0.2965954673551001730, 5.229263513284051257, -5.108749999999999680 ) ) ;
#2430=ORIENTED_EDGE ( 'NONE', *, *, #2367, .T. ) ;
#2434=ORIENTED_EDGE ( 'NONE', *, *, #3285, .T. ) ;
#2439=VERTEX_POINT ( 'NONE', #11 ) ;
#2446=EDGE_CURVE ( 'NONE', #3785, #47, #6218, .T. ) ;
#2450=CARTESIAN_POINT ( 'NONE',  ( -1.198957880828181333, 2.500000000000000000, -2.750000000000000444 ) ) ;
#2451=CARTESIAN_POINT ( 'NONE',  ( 0.7335700393700786970, 2.500000000000000444, 2.909883779527559611 ) ) ;
#2454=CARTESIAN_POINT ( 'NONE',  ( 1.249999999999999556, 3.950000000000000178, 3.691250000234376660 ) ) ;
#2456=VECTOR ( 'NONE', #4425, 39.37007874015748143 ) ;
#2457=CIRCLE ( 'NONE', #7318, 3.000000000518587839 ) ;
#2473=VERTEX_POINT ( 'NONE', #8167 ) ;
#2485=CARTESIAN_POINT ( 'NONE',  ( 1.986718228346456838, 3.767850944881891095, -4.887177007874016432 ) ) ;
#2489=ORIENTED_EDGE ( 'NONE', *, *, #3708, .T. ) ;
#2495=ORIENTED_EDGE ( 'NONE', *, *, #5261, .F. ) ;
#2500=EDGE_CURVE ( 'NONE', #3620, #3785, #2177, .T. ) ;
#2501=CARTESIAN_POINT ( 'NONE',  ( 3.296097361251832503, 1.749999999892448477, 0.5624999982029994516 ) ) ;
#2502=CARTESIAN_POINT ( 'NONE',  ( 1.625000000000000222, 2.500000000000000000, -2.521780125229002412 ) ) ;
#2503=DIRECTION ( 'NONE',  ( -0.000000000000000000, -0.000000000000000000, 1.000000000000000000 ) ) ;
#2511=PLANE ( 'NONE',  #314 ) ;
#2514=ORIENTED_EDGE ( 'NONE', *, *, #1538, .F. ) ;
#2516=CARTESIAN_POINT ( 'NONE',  ( -0.2278784911965701654, 2.340730451631669151, -3.064708773258130847 ) ) ;
#2518=CARTESIAN_POINT ( 'NONE',  ( 1.213899189620355035, 3.445445541707729653, -5.108749999999997904 ) ) ;
#2519=CARTESIAN_POINT ( 'NONE',  ( -1.500000000000000444, 5.113999999999999879, 2.749999998413802160 ) ) ;
#2526=CARTESIAN_POINT ( 'NONE',  ( -2.749999999999999556, 7.339000000000001300, 3.161250000000001670 ) ) ;
#2530=VECTOR ( 'NONE', #7240, 39.37007874015748143 ) ;
#2531=DIRECTION ( 'NONE',  ( -0.000000000000000000, 1.000000000000000000, -0.000000000000000000 ) ) ;
#2535=DIRECTION ( 'NONE',  ( -0.000000000000000000, -0.000000000000000000, 1.000000000000000000 ) ) ;
#2536=EDGE_CURVE ( 'NONE', #691, #5594, #7375, .T. ) ;
#2538=AXIS2_PLACEMENT_3D ( 'NONE', #1696, #6585, #957 ) ;
#2541=DIRECTION ( 'NONE',  ( 0.000000000000000000, 0.000000000000000000, 1.000000000000000000 ) ) ;
#2543=CARTESIAN_POINT ( 'NONE',  ( 0.000000000000000000, 1.750000000000000444, 2.693920355039552791E-42 ) ) ;
#2550=DIRECTION ( 'NONE',  ( 0.000000000000000000, 0.000000000000000000, -1.000000000000000000 ) ) ;
#2553=DIRECTION ( 'NONE',  ( -0.000000000000000000, -0.000000000000000000, 1.000000000000000000 ) ) ;
#2556=ORIENTED_EDGE ( 'NONE', *, *, #6831, .T. ) ;
#2559=CARTESIAN_POINT ( 'NONE',  ( 0.8008852451031778230, 4.990709419004156544, -5.108750000000001457 ) ) ;
#2561=ORIENTED_EDGE ( 'NONE', *, *, #5261, .T. ) ;
#2565=ORIENTED_EDGE ( 'NONE', *, *, #2731, .T. ) ;
#2569=DIRECTION ( 'NONE',  ( 1.000000000000000000, 0.000000000000000000, 0.000000000000000000 ) ) ;
#2570=DIRECTION ( 'NONE',  ( -0.000000000000000000, -1.000000000000000000, 0.000000000000000000 ) ) ;
#2577=AXIS2_PLACEMENT_3D ( 'NONE', #395, #7341, #5381 ) ;
#2579=CARTESIAN_POINT ( 'NONE',  ( 3.479221556377631263E-16, 1.664000000000000368, -2.841000000000000636 ) ) ;
#2583=CARTESIAN_POINT ( 'NONE',  ( 2.750000000000000444, 7.541160346212514298, 3.714531354832316445 ) ) ;
#2588=ORIENTED_EDGE ( 'NONE', *, *, #3163, .T. ) ;
#2589=CARTESIAN_POINT ( 'NONE',  ( -2.078417272059708142E-11, 3.950000000000000178, 2.749999998413802160 ) ) ;
#2595=ORIENTED_EDGE ( 'NONE', *, *, #4641, .T. ) ;
#2599=CARTESIAN_POINT ( 'NONE',  ( 0.8651000694493629073, 2.962007182104931413, -5.108749999999997904 ) ) ;
#2601=ORIENTED_EDGE ( 'NONE', *, *, #3921, .T. ) ;
#2612=CARTESIAN_POINT ( 'NONE',  ( -2.537500000000000533, 1.664000000000000368, 0.2625000000000008438 ) ) ;
#2613=DIRECTION ( 'NONE',  ( 1.000000000000000000, 0.000000000000000000, 0.000000000000000000 ) ) ;
#2618=CARTESIAN_POINT ( 'NONE',  ( 1.500000000000000444, 5.113999999999999879, 0.000000000000000000 ) ) ;
#2625=CARTESIAN_POINT ( 'NONE',  ( 2.750000000000002665, 7.963999999999999524, 2.411250000000000338 ) ) ;
#2627=DIRECTION ( 'NONE',  ( 0.000000000000000000, 0.000000000000000000, -1.000000000000000000 ) ) ;
#2634=EDGE_CURVE ( 'NONE', #3785, #674, #2457, .T. ) ;
#2636=ORIENTED_EDGE ( 'NONE', *, *, #1427, .F. ) ;
#2638=ADVANCED_FACE ( 'NONE', ( #1553 ), #3391, .T. ) ;
#2640=CARTESIAN_POINT ( 'NONE',  ( 1.205291313024512867, 4.469991316918233260, -5.108749999999997904 ) ) ;
#2641=CARTESIAN_POINT ( 'NONE',  ( 0.000000000000000000, 3.950000000000000178, 3.691250000234376660 ) ) ;
#2643=DIRECTION ( 'NONE',  ( 1.000000000000000000, 0.000000000000000000, -0.000000000000000000 ) ) ;
#2647=EDGE_CURVE ( 'NONE', #6784, #6962, #6426, .T. ) ;
#2648=DIRECTION ( 'NONE',  ( 1.000000000000000000, 0.000000000000000000, 0.000000000000000000 ) ) ;
#2653=CYLINDRICAL_SURFACE ( 'NONE', #195, 1.249999999999999556 ) ;
#2671=CARTESIAN_POINT ( 'NONE',  ( -2.750000000000000888, 8.589000000000000412, 3.243476614173229411 ) ) ;
#2677=DIRECTION ( 'NONE',  ( -1.000000000000000000, 0.000000000000000000, -0.000000000000000000 ) ) ;
#2678=VERTEX_POINT ( 'NONE', #2118 ) ;
#2679=AXIS2_PLACEMENT_3D ( 'NONE', #6401, #6441, #6932 ) ;
#2683=AXIS2_PLACEMENT_3D ( 'NONE', #2824, #1602, #5229 ) ;
#2684=EDGE_CURVE ( 'NONE', #4928, #3352, #4611, .T. ) ;
#2686=EDGE_CURVE ( 'NONE', #2392, #1952, #6018, .T. ) ;
#2687=ADVANCED_FACE ( 'NONE', ( #6011 ), #2927, .F. ) ;
#2693=PLANE ( 'NONE',  #850 ) ;
#2694=ORIENTED_EDGE ( 'NONE', *, *, #4224, .F. ) ;
#2698=LINE ( 'NONE', #189, #560 ) ;
#2704=AXIS2_PLACEMENT_3D ( 'NONE', #2641, #1373, #124 ) ;
#2706=VERTEX_POINT ( 'NONE', #4817 ) ;
#2712=CARTESIAN_POINT ( 'NONE',  ( -1.168432152159266657, 3.351763300421212399, -5.108749999999997904 ) ) ;
#2715=CARTESIAN_POINT ( 'NONE',  ( -1.201750196850394081, 2.500000000000000444, -0.5625000000000003331 ) ) ;
#2718=CARTESIAN_POINT ( 'NONE',  ( -3.296097360993826886, 2.500000000000000444, 0.5625000000000001110 ) ) ;
#2723=ORIENTED_EDGE ( 'NONE', *, *, #1694, .T. ) ;
#2725=EDGE_CURVE ( 'NONE', #2302, #7663, #6833, .T. ) ;
#2726=CARTESIAN_POINT ( 'NONE',  ( 0.000000000000000000, 2.499999999857933197, 0.000000000000000000 ) ) ;
#2731=EDGE_CURVE ( 'NONE', #6240, #1632, #4136, .T. ) ;
#2736=ORIENTED_EDGE ( 'NONE', *, *, #6294, .F. ) ;
#2737=DIRECTION ( 'NONE',  ( -0.000000000000000000, -0.000000000000000000, 1.000000000000000000 ) ) ;
#2739=ORIENTED_EDGE ( 'NONE', *, *, #3582, .T. ) ;
#2740=CARTESIAN_POINT ( 'NONE',  ( 3.296097360985625002, 2.500000000000000444, -0.5625000000000001110 ) ) ;
#2743=CARTESIAN_POINT ( 'NONE',  ( 1.625000000000000222, 3.950000000000000178, 2.750000000234376074 ) ) ;
#2747=CARTESIAN_POINT ( 'NONE',  ( -1.261644052163539920, 4.312451747426980120, -5.108749999999998792 ) ) ;
#2748=DIRECTION ( 'NONE',  ( -1.000000000000000000, 0.000000000000000000, -0.000000000000000000 ) ) ;
#2749=CARTESIAN_POINT ( 'NONE',  ( 2.750000000000000444, 7.339000000000003077, 2.411250000000000338 ) ) ;
#2750=PLANE ( 'NONE',  #3195 ) ;
#2755=CARTESIAN_POINT ( 'NONE',  ( 0.000000000000000000, 1.664000000000000368, 2.693920355039552791E-42 ) ) ;
#2757=ORIENTED_EDGE ( 'NONE', *, *, #7788, .F. ) ;
#2767=LINE ( 'NONE', #5252, #7568 ) ;
#2768=EDGE_CURVE ( 'NONE', #4783, #2678, #8002, .T. ) ;
#2770=DIRECTION ( 'NONE',  ( 1.000000000000000000, 0.000000000000000000, 0.000000000000000000 ) ) ;
#2771=CARTESIAN_POINT ( 'NONE',  ( 1.312500000123273169, 7.352492868468935683, 3.316250000424603606 ) ) ;
#2773=DIRECTION ( 'NONE',  ( 0.000000000000000000, 0.000000000000000000, -1.000000000000000000 ) ) ;
#2781=ORIENTED_EDGE ( 'NONE', *, *, #6281, .T. ) ;
#2784=EDGE_CURVE ( 'NONE', #3627, #3267, #3731, .T. ) ;
#2785=CARTESIAN_POINT ( 'NONE',  ( -0.6955818286634507519, 2.836155590436416851, -5.108750000000003233 ) ) ;
#2786=CARTESIAN_POINT ( 'NONE',  ( -0.7631207261360639649, 5.018067241527451650, -5.108749999999999680 ) ) ;
#2788=CARTESIAN_POINT ( 'NONE',  ( 2.750000000000000888, 8.574153543307089009, 3.323750000000001315 ) ) ;
#2789=( NAMED_UNIT ( * ) PLANE_ANGLE_UNIT ( ) SI_UNIT ( $, .RADIAN. ) );
#2795=DIRECTION ( 'NONE',  ( 0.000000000000000000, 0.000000000000000000, 1.000000000000000000 ) ) ;
#2806=VECTOR ( 'NONE', #2220, 39.37007874015748143 ) ;
#2807=EDGE_CURVE ( 'NONE', #2981, #1998, #1803, .T. ) ;
#2808=VECTOR ( 'NONE', #5571, 39.37007874015748143 ) ;
#2809=CARTESIAN_POINT ( 'NONE',  ( 1.500000000000000444, 5.639000000000001123, 0.5414159055118110686 ) ) ;
#2811=( GEOMETRIC_REPRESENTATION_CONTEXT ( 3 ) GLOBAL_UNCERTAINTY_ASSIGNED_CONTEXT ( ( #3889 ) ) GLOBAL_UNIT_ASSIGNED_CONTEXT ( ( #908, #2789, #7225 ) ) REPRESENTATION_CONTEXT ( 'NONE', 'WORKASPACE' ) );
#2821=ORIENTED_EDGE ( 'NONE', *, *, #3137, .F. ) ;
#2824=CARTESIAN_POINT ( 'NONE',  ( 0.000000000000000000, 2.500000000130568889, 0.000000000000000000 ) ) ;
#2826=VERTEX_POINT ( 'NONE', #59 ) ;
#2828=CARTESIAN_POINT ( 'NONE',  ( -1.116010548110457856, 3.257898045036971002, -5.108750000000001457 ) ) ;
#2832=CARTESIAN_POINT ( 'NONE',  ( 1.624999999905518688, 3.950000000000000178, 2.749999999885571533 ) ) ;
#2833=AXIS2_PLACEMENT_3D ( 'NONE', #5223, #7769, #734 ) ;
#2835=ORIENTED_EDGE ( 'NONE', *, *, #3251, .T. ) ;
#2839=AXIS2_PLACEMENT_3D ( 'NONE', #4195, #7386, #3786 ) ;
#2840=AXIS2_PLACEMENT_3D ( 'NONE', #2718, #5206, #2677 ) ;
#2842=CARTESIAN_POINT ( 'NONE',  ( -3.343750000000001776, 1.750000000000000444, 0.5625000000000003331 ) ) ;
#2844=CARTESIAN_POINT ( 'NONE',  ( -0.7335700382782335272, 2.500000000365355302, -5.108750000000001457 ) ) ;
#2847=PLANE ( 'NONE',  #5179 ) ;
#2851=LINE ( 'NONE', #3512, #1243 ) ;
#2858=PLANE ( 'NONE',  #1246 ) ;
#2863=FACE_OUTER_BOUND ( 'NONE', #4049, .T. ) ;
#2867=DIRECTION ( 'NONE',  ( -1.000000000000000000, -0.000000000000000000, 0.000000000000000000 ) ) ;
#2868=CARTESIAN_POINT ( 'NONE',  ( -0.2166615117570589999, 2.654796885154087516, -5.108749999999997904 ) ) ;
#2871=LINE ( 'NONE', #863, #3591 ) ;
#2872=CARTESIAN_POINT ( 'NONE',  ( -1.312500000000000444, 7.352492870354978116, 3.316250000370397188 ) ) ;
#2874=EDGE_LOOP ( 'NONE', ( #3303, #359, #8000, #3343 ) ) ;
#2875=ADVANCED_FACE ( 'NONE', ( #3761 ), #3184, .F. ) ;
#2878=CARTESIAN_POINT ( 'NONE',  ( -2.537500000000000533, 2.500000000000000444, -0.2625000000000008438 ) ) ;
#2884=FACE_OUTER_BOUND ( 'NONE', #3624, .T. ) ;
#2891=DIRECTION ( 'NONE',  ( 0.000000000000000000, 0.000000000000000000, -1.000000000000000000 ) ) ;
#2892=DIRECTION ( 'NONE',  ( 0.000000000000000000, -1.000000000000000000, 0.000000000000000000 ) ) ;
#2895=ORIENTED_EDGE ( 'NONE', *, *, #7186, .F. ) ;
#2896=DIRECTION ( 'NONE',  ( -0.000000000000000000, 0.000000000000000000, -1.000000000000000000 ) ) ;
#2901=CARTESIAN_POINT ( 'NONE',  ( 0.000000000000000000, 3.950000000000000178, 3.691250000234376216 ) ) ;
#2917=EDGE_CURVE ( 'NONE', #1059, #2209, #4331, .T. ) ;
#2922=ORIENTED_EDGE ( 'NONE', *, *, #6989, .T. ) ;
#2924=VECTOR ( 'NONE', #5452, 39.37007874015748143 ) ;
#2927=PLANE ( 'NONE',  #2577 ) ;
#2931=ORIENTED_EDGE ( 'NONE', *, *, #7197, .T. ) ;
#2933=EDGE_CURVE ( 'NONE', #843, #7238, #3427, .T. ) ;
#2934=FACE_OUTER_BOUND ( 'NONE', #319, .T. ) ;
#2935=ORIENTED_EDGE ( 'NONE', *, *, #177, .F. ) ;
#2937=ORIENTED_EDGE ( 'NONE', *, *, #5242, .F. ) ;
#2939=PLANE ( 'NONE',  #7006 ) ;
#2944=LINE ( 'NONE', #6106, #880 ) ;
#2947=CARTESIAN_POINT ( 'NONE',  ( 0.03134105979970094186, 2.325218920766706887, 3.079992493227982298 ) ) ;
#2948=AXIS2_PLACEMENT_3D ( 'NONE', #5132, #3787, #7678 ) ;
#2956=CIRCLE ( 'NONE', #7839, 1.624999999999999778 ) ;
#2957=FACE_OUTER_BOUND ( 'NONE', #7468, .T. ) ;
#2964=VECTOR ( 'NONE', #892, 39.37007874015748143 ) ;
#2966=LINE ( 'NONE', #4226, #5930 ) ;
#2971=ORIENTED_EDGE ( 'NONE', *, *, #887, .T. ) ;
#2972=AXIS2_PLACEMENT_3D ( 'NONE', #5831, #1570, #1534 ) ;
#2974=DIRECTION ( 'NONE',  ( -1.000000000000000000, 0.000000000000000000, -0.000000000000000000 ) ) ;
#2975=( BOUNDED_SURFACE ( )  B_SPLINE_SURFACE ( 2, 1, ( 
 ( #2788, #156 ),
 ( #5825, #2671 ),
 ( #1444, #2059 ),
 ( #3321, #208 ),
 ( #7746, #7099 ),
 ( #2749, #1481 ),
 ( #6491, #5236 ),
 ( #7831, #6029 ),
 ( #414, #1034 ),
 ( #5570, #1964 ),
 ( #2583, #7611 ) ),
 .UNSPECIFIED., .F., .F., .F. ) 
 B_SPLINE_SURFACE_WITH_KNOTS ( ( 3, 2, 2, 2, 2, 3 ),
 ( 2, 2 ),
 ( 1.337827206813319902, 1.570796326794899889, 3.141592653589790007, 4.712388980384690562, 5.497197239955569081, 5.538790940286991926 ),
 ( 0.000000000000000000, 1.000000000000000000 ),
 .UNSPECIFIED. ) 
 GEOMETRIC_REPRESENTATION_ITEM ( )  RATIONAL_B_SPLINE_SURFACE ( (
 ( 0.9260057553135151442, 0.9260057553135151442),
 ( 0.9565602018087399072, 0.9565602018087399072),
 ( 1.000000000000000000, 1.000000000000000000),
 ( 0.7071067811865479058, 0.7071067811865479058),
 ( 1.000000000000000000, 1.000000000000000000),
 ( 0.7071067811865479058, 0.7071067811865479058),
 ( 1.000000000000000000, 1.000000000000000000),
 ( 0.8536633850130519452, 0.8536633850130519452),
 ( 0.8535534732088591037, 0.8535534732088591037),
 ( 0.8535534732088591037, 0.8535534732088591037),
 ( 0.8535534732088591037, 0.8535534732088591037) ) ) 
 REPRESENTATION_ITEM ( '' )  SURFACE ( )  );
#2981=VERTEX_POINT ( 'NONE', #2612 ) ;
#2983=CARTESIAN_POINT ( 'NONE',  ( 1.274606805354365768, 2.434036455968486834, 2.749999999536767437 ) ) ;
#2990=CARTESIAN_POINT ( 'NONE',  ( 1.312500000061636696, 4.908106857212807483, 2.750000000234376074 ) ) ;
#2991=EDGE_CURVE ( 'NONE', #2473, #417, #2698, .T. ) ;
#2994=FACE_OUTER_BOUND ( 'NONE', #8097, .T. ) ;
#2995=ORIENTED_EDGE ( 'NONE', *, *, #5095, .F. ) ;
#2998=CARTESIAN_POINT ( 'NONE',  ( 3.343750000000001776, 2.500000000000000444, 2.909883779527559611 ) ) ;
#3002=DIRECTION ( 'NONE',  ( 0.000000000000000000, -1.000000000000000000, 0.000000000000000000 ) ) ;
#3003=FACE_BOUND ( 'NONE', #7013, .T. ) ;
#3004=VERTEX_POINT ( 'NONE', #6519 ) ;
#3012=ADVANCED_FACE ( 'NONE', ( #3869 ), #5219, .T. ) ;
#3018=CARTESIAN_POINT ( 'NONE',  ( 0.7335700383277801162, 2.500000000390421473, -2.908930215353081383 ) ) ;
#3021=ORIENTED_EDGE ( 'NONE', *, *, #5752, .T. ) ;
#3032=LINE ( 'NONE', #1079, #5269 ) ;
#3033=CARTESIAN_POINT ( 'NONE',  ( 1.312500000000000444, 5.969165905511811587, 0.5414159055118111796 ) ) ;
#3035=ORIENTED_EDGE ( 'NONE', *, *, #4661, .T. ) ;
#3037=CARTESIAN_POINT ( 'NONE',  ( 3.063407152847613446, 2.250083286476321831, -0.5624999999737114731 ) ) ;
#3040=CARTESIAN_POINT ( 'NONE',  ( -1.465509921259843251, 2.890529173228346682, -7.381560866141734678 ) ) ;
#3041=CARTESIAN_POINT ( 'NONE',  ( 2.187663376927555706E-18, 3.950000000000000178, 0.5414159055118110686 ) ) ;
#3046=AXIS2_PLACEMENT_3D ( 'NONE', #4885, #6041, #6629 ) ;
#3050=VECTOR ( 'NONE', #7430, 39.37007874015748143 ) ;
#3061=VECTOR ( 'NONE', #5932, 39.37007874015748143 ) ;
#3063=CARTESIAN_POINT ( 'NONE',  ( 1.624999999999999556, 2.076218724953421191, -2.749999999536766992 ) ) ;
#3075=ORIENTED_EDGE ( 'NONE', *, *, #1821, .T. ) ;
#3077=AXIS2_PLACEMENT_3D ( 'NONE', #5350, #939, #3522 ) ;
#3079=DIRECTION ( 'NONE',  ( -0.000000000000000000, 1.000000000000000000, 0.000000000000000000 ) ) ;
#3084=CARTESIAN_POINT ( 'NONE',  ( 0.8969582018468957862, 2.990857292758699160, -5.108750000000002345 ) ) ;
#3090=ORIENTED_EDGE ( 'NONE', *, *, #3243, .T. ) ;
#3091=ORIENTED_EDGE ( 'NONE', *, *, #3819, .T. ) ;
#3094=DIRECTION ( 'NONE',  ( -0.000000000000000000, 0.000000000000000000, -1.000000000000000000 ) ) ;
#3097=FACE_OUTER_BOUND ( 'NONE', #2394, .T. ) ;
#3101=DIRECTION ( 'NONE',  ( -0.000000000000000000, 1.000000000000000000, -0.000000000000000000 ) ) ;
#3107=ORIENTED_EDGE ( 'NONE', *, *, #1821, .F. ) ;
#3111=CARTESIAN_POINT ( 'NONE',  ( 0.7335700393700786970, 2.500000000000000444, 0.5625000000000001110 ) ) ;
#3113=FACE_OUTER_BOUND ( 'NONE', #6816, .T. ) ;
#3116=ORIENTED_EDGE ( 'NONE', *, *, #337, .F. ) ;
#3122=SHAPE_DEFINITION_REPRESENTATION ( #4249, #6505 ) ;
#3128=ORIENTED_EDGE ( 'NONE', *, *, #4927, .T. ) ;
#3130=EDGE_CURVE ( 'NONE', #1364, #5899, #593, .T. ) ;
#3131=CARTESIAN_POINT ( 'NONE',  ( 0.000000000000000000, 5.639000000000001123, 0.1249999999999997641 ) ) ;
#3132=CARTESIAN_POINT ( 'NONE',  ( 1.136188160977859019, 3.292580994510421633, -5.108750000000003233 ) ) ;
#3133=CARTESIAN_POINT ( 'NONE',  ( 0.000000000000000000, 1.749999999911819204, 0.000000000000000000 ) ) ;
#3137=EDGE_CURVE ( 'NONE', #3703, #2223, #2966, .T. ) ;
#3145=CARTESIAN_POINT ( 'NONE',  ( 1.198957881890679422, 2.500000000000000000, 2.749999999536767437 ) ) ;
#3154=DIRECTION ( 'NONE',  ( -0.000000000000000000, 1.000000000000000000, 0.000000000000000000 ) ) ;
#3163=EDGE_CURVE ( 'NONE', #3439, #7577, #4307, .T. ) ;
#3165=CARTESIAN_POINT ( 'NONE',  ( 1.044888736288899667, 4.748860047246612481, -5.108750000000002345 ) ) ;
#3167=ORIENTED_EDGE ( 'NONE', *, *, #7634, .T. ) ;
#3171=ADVANCED_FACE ( 'NONE', ( #1695 ), #8141, .T. ) ;
#3172=VECTOR ( 'NONE', #3586, 39.37007874015748143 ) ;
#3175=DIRECTION ( 'NONE',  ( 1.000000000000000000, 0.000000000000000000, 0.000000000000000000 ) ) ;
#3184=CYLINDRICAL_SURFACE ( 'NONE', #1875, 1.249999999999999556 ) ;
#3189=CARTESIAN_POINT ( 'NONE',  ( 0.000000000000000000, 3.950000000000000178, -2.750000000000000444 ) ) ;
#3195=AXIS2_PLACEMENT_3D ( 'NONE', #7473, #3884, #4428 ) ;
#3197=ORIENTED_EDGE ( 'NONE', *, *, #4218, .F. ) ;
#3199=CARTESIAN_POINT ( 'NONE',  ( -1.500000000000000444, 5.113999999999999879, -2.750000000000000444 ) ) ;
#3202=CARTESIAN_POINT ( 'NONE',  ( 1.500000000000000444, 5.414000000000000590, 0.5414159055118110686 ) ) ;
#3204=ORIENTED_EDGE ( 'NONE', *, *, #3280, .T. ) ;
#3208=CARTESIAN_POINT ( 'NONE',  ( 1.295380378688662182, 4.162394200796177834, -5.108750000000002345 ) ) ;
#3209=CARTESIAN_POINT ( 'NONE',  ( -1.500000000000000444, 5.339000000000000412, -2.750000000000000444 ) ) ;
#3212=LINE ( 'NONE', #716, #5714 ) ;
#3216=CARTESIAN_POINT ( 'NONE',  ( -1.201750196850394081, 2.500000000000000444, 0.5625000000000003331 ) ) ;
#3225=AXIS2_PLACEMENT_3D ( 'NONE', #3471, #3995, #353 ) ;
#3226=VERTEX_POINT ( 'NONE', #225 ) ;
#3237=LINE ( 'NONE', #4504, #7037 ) ;
#3243=EDGE_CURVE ( 'NONE', #811, #3703, #2405, .T. ) ;
#3245=B_SPLINE_CURVE_WITH_KNOTS ( 'NONE', 3,
 ( #7263, #1641, #4124, #6177 ),
 .UNSPECIFIED., .F., .F.,
 ( 4, 4 ),
 ( 0.000000000000000000, 0.01222568465131274387 ),
 .UNSPECIFIED. ) ;
#3248=CARTESIAN_POINT ( 'NONE',  ( 0.3427223730929865875, 5.219860580395915051, -5.108749999999999680 ) ) ;
#3249=CARTESIAN_POINT ( 'NONE',  ( 0.6796608066838680795, 2.472726760981024174, -2.935416550745896469 ) ) ;
#3250=CYLINDRICAL_SURFACE ( 'NONE', #3993, 1.624999995942718156 ) ;
#3251=EDGE_CURVE ( 'NONE', #7586, #6784, #1580, .T. ) ;
#3252=VERTEX_POINT ( 'NONE', #250 ) ;
#3257=FACE_OUTER_BOUND ( 'NONE', #3738, .T. ) ;
#3259=EDGE_LOOP ( 'NONE', ( #1894, #2175, #8174, #2937, #469, #4704, #2101, #4422 ) ) ;
#3266=CARTESIAN_POINT ( 'NONE',  ( 0.000000000000000000, 2.500000000000000000, 0.000000000000000000 ) ) ;
#3267=VERTEX_POINT ( 'NONE', #5233 ) ;
#3272=ORIENTED_EDGE ( 'NONE', *, *, #2339, .T. ) ;
#3280=EDGE_CURVE ( 'NONE', #6942, #95, #2173, .T. ) ;
#3281=DIRECTION ( 'NONE',  ( 0.000000000000000000, 0.000000000000000000, -1.000000000000000000 ) ) ;
#3282=FACE_BOUND ( 'NONE', #653, .T. ) ;
#3284=EDGE_LOOP ( 'NONE', ( #5257, #7845, #4930, #5874, #5, #3297 ) ) ;
#3285=EDGE_CURVE ( 'NONE', #7385, #5858, #6651, .T. ) ;
#3287=ORIENTED_EDGE ( 'NONE', *, *, #1538, .T. ) ;
#3289=EDGE_CURVE ( 'NONE', #6623, #1945, #1746, .T. ) ;
#3291=CARTESIAN_POINT ( 'NONE',  ( 0.6588840751933063844, 5.085949231003589865, -5.108749999999999680 ) ) ;
#3294=ADVANCED_FACE ( 'NONE', ( #4127, #3360, #1643 ), #206, .T. ) ;
#3295=CARTESIAN_POINT ( 'NONE',  ( -1.312500000000000444, 4.908106850393701315, 2.749999992430256945 ) ) ;
#3297=ORIENTED_EDGE ( 'NONE', *, *, #2725, .T. ) ;
#3303=ORIENTED_EDGE ( 'NONE', *, *, #6123, .T. ) ;
#3317=AXIS2_PLACEMENT_3D ( 'NONE', #3830, #6219, #610 ) ;
#3321=CARTESIAN_POINT ( 'NONE',  ( 2.750000000000000444, 8.589000000000000412, 2.411250000000000338 ) ) ;
#3324=CARTESIAN_POINT ( 'NONE',  ( 2.537500000000000533, 2.500000000000000444, -0.2625000000000008438 ) ) ;
#3331=DIRECTION ( 'NONE',  ( 0.000000000000000000, 0.000000000000000000, 1.000000000000000000 ) ) ;
#3335=VECTOR ( 'NONE', #7173, 39.37007874015748143 ) ;
#3339=VECTOR ( 'NONE', #5096, 39.37007874015748143 ) ;
#3341=DIRECTION ( 'NONE',  ( 1.000000000000000000, 0.000000000000000000, 0.000000000000000000 ) ) ;
#3343=ORIENTED_EDGE ( 'NONE', *, *, #4218, .T. ) ;
#3349=VECTOR ( 'NONE', #2569, 39.37007874015748143 ) ;
#3352=VERTEX_POINT ( 'NONE', #6836 ) ;
#3353=EDGE_CURVE ( 'NONE', #4996, #3433, #1183, .T. ) ;
#3357=CARTESIAN_POINT ( 'NONE',  ( -2.078417272059708142E-11, 5.414000000000000590, 2.749999998413802160 ) ) ;
#3359=ORIENTED_EDGE ( 'NONE', *, *, #19, .F. ) ;
#3360=FACE_BOUND ( 'NONE', #7819, .T. ) ;
#3361=CARTESIAN_POINT ( 'NONE',  ( 0.7052155605301346775, 5.414000000000000590, 0.000000000000000000 ) ) ;
#3362=FACE_OUTER_BOUND ( 'NONE', #4830, .T. ) ;
#3368=CARTESIAN_POINT ( 'NONE',  ( 0.000000000000000000, 1.749999999911819204, -3.343750000040417447 ) ) ;
#3378=VERTEX_POINT ( 'NONE', #5564 ) ;
#3380=EDGE_CURVE ( 'NONE', #4179, #4298, #6721, .T. ) ;
#3383=EDGE_CURVE ( 'NONE', #2271, #7545, #1109, .T. ) ;
#3391=PLANE ( 'NONE',  #3225 ) ;
#3401=CARTESIAN_POINT ( 'NONE',  ( 1.249999999999999556, 3.950000000000000178, 3.691250000234376660 ) ) ;
#3404=B_SPLINE_CURVE_WITH_KNOTS ( 'NONE', 3,
 ( #5934, #357, #5264, #5227 ),
 .UNSPECIFIED., .F., .F.,
 ( 4, 4 ),
 ( 0.000000000000000000, 0.01222568467003884961 ),
 .UNSPECIFIED. ) ;
#3406=CARTESIAN_POINT ( 'NONE',  ( -1.625000000000000222, 5.113999999999999879, 2.750000000000000444 ) ) ;
#3407=( BOUNDED_SURFACE ( )  B_SPLINE_SURFACE ( 3, 3, ( 
 ( #8150, #3432, #542, #1823 ),
 ( #4314, #7336, #7377, #8063 ),
 ( #2485, #1705, #3040, #594 ),
 ( #4969, #3631, #7510, #2398 ) ),
 .UNSPECIFIED., .F., .F., .T. ) 
 B_SPLINE_SURFACE_WITH_KNOTS ( ( 4, 4 ),
 ( 4, 4 ),
 ( 0.000000000000000000, 1.000000000000000000 ),
 ( 0.000000000000000000, 1.000000000000000000 ),
 .UNSPECIFIED. ) 
 GEOMETRIC_REPRESENTATION_ITEM ( )  RATIONAL_B_SPLINE_SURFACE ( (
 ( 1.000000000000000000, 0.4766096016200470631, 0.4766096016200470631, 1.000000000000000000),
 ( 0.6249252401552001235, 0.2978453697526821098, 0.2978453697526821098, 0.6249252401552001235),
 ( 0.6249252401552001235, 0.2978453697526821098, 0.2978453697526821098, 0.6249252401552001235),
 ( 1.000000000000000000, 0.4766096016200470631, 0.4766096016200470631, 1.000000000000000000) ) ) 
 REPRESENTATION_ITEM ( '' )  SURFACE ( )  );
#3412=PLANE ( 'NONE',  #2840 ) ;
#3418=ORIENTED_EDGE ( 'NONE', *, *, #3749, .T. ) ;
#3425=DIRECTION ( 'NONE',  ( 0.000000000000000000, 1.000000000000000000, -0.000000000000000000 ) ) ;
#3427=LINE ( 'NONE', #847, #1618 ) ;
#3432=CARTESIAN_POINT ( 'NONE',  ( 0.1186214960629921461, 5.264455944881891725, -5.098178543307088972 ) ) ;
#3433=VERTEX_POINT ( 'NONE', #4295 ) ;
#3434=DIRECTION ( 'NONE',  ( -0.000000000000000000, 1.000000000000000000, -0.000000000000000000 ) ) ;
#3439=VERTEX_POINT ( 'NONE', #3063 ) ;
#3440=CARTESIAN_POINT ( 'NONE',  ( -0.08551597065243228546, 5.262577827926121721, -5.108750000000001457 ) ) ;
#3442=CARTESIAN_POINT ( 'NONE',  ( -1.044888770141576328, 3.151139990177239447, -5.108750000000002345 ) ) ;
#3443=CARTESIAN_POINT ( 'NONE',  ( 0.06423988825481448395, 2.326186878295140481, 3.079038241297371137 ) ) ;
#3444=LINE ( 'NONE', #3406, #2806 ) ;
#3445=DIRECTION ( 'NONE',  ( -0.000000000000000000, -1.000000000000000000, 0.000000000000000000 ) ) ;
#3449=CARTESIAN_POINT ( 'NONE',  ( -1.624999999999999778, 3.950000000000000178, -5.108750000000001457 ) ) ;
#3451=AXIS2_PLACEMENT_3D ( 'NONE', #7842, #7923, #2260 ) ;
#3452=CIRCLE ( 'NONE', #7541, 1.249999999999999556 ) ;
#3457=VECTOR ( 'NONE', #3666, 39.37007874015748143 ) ;
#3465=CARTESIAN_POINT ( 'NONE',  ( 0.3224709391354322330, 2.356032306969389367, -3.049642098122674838 ) ) ;
#3466=CARTESIAN_POINT ( 'NONE',  ( -3.343750000000001776, 0.000000000000000000, 0.000000000000000000 ) ) ;
#3469=CARTESIAN_POINT ( 'NONE',  ( 1.625000000000000222, 5.113999999999999879, -2.750000000000000444 ) ) ;
#3471=CARTESIAN_POINT ( 'NONE',  ( 0.000000000000000000, 5.151388682096968097, 2.750000000000000444 ) ) ;
#3472=VECTOR ( 'NONE', #569, 39.37007874015748143 ) ;
#3473=CARTESIAN_POINT ( 'NONE',  ( 2.750000000000002665, 8.589000000000000412, 3.243476614173228967 ) ) ;
#3476=VERTEX_POINT ( 'NONE', #6799 ) ;
#3477=CARTESIAN_POINT ( 'NONE',  ( -2.537500000000000533, 1.664000000000000368, -0.2625000000000008438 ) ) ;
#3483=AXIS2_PLACEMENT_3D ( 'NONE', #5059, #7598, #1949 ) ;
#3487=ORIENTED_EDGE ( 'NONE', *, *, #1245, .F. ) ;
#3489=CARTESIAN_POINT ( 'NONE',  ( -1.291725147455078382, 3.716413631672734752, -5.108749999999998792 ) ) ;
#3490=CARTESIAN_POINT ( 'NONE',  ( 0.2590873717497497175, 2.344476708467012394, 3.061018729179389997 ) ) ;
#3500=DIRECTION ( 'NONE',  ( 0.000000000000000000, -0.000000000000000000, 1.000000000000000000 ) ) ;
#3507=ADVANCED_FACE ( 'NONE', ( #6685 ), #1069, .T. ) ;
#3512=CARTESIAN_POINT ( 'NONE',  ( 2.750000000000000444, 7.964000000000000412, 3.691250000000001030 ) ) ;
#3514=CARTESIAN_POINT ( 'NONE',  ( 1.312500000000000444, 7.339000000000003077, 2.411250000000000782 ) ) ;
#3516=CARTESIAN_POINT ( 'NONE',  ( 0.000000000000000000, 1.749999999911819204, 0.000000000000000000 ) ) ;
#3517=EDGE_LOOP ( 'NONE', ( #6292, #161, #5716, #5314 ) ) ;
#3522=DIRECTION ( 'NONE',  ( 1.000000000000000000, 0.000000000000000000, 0.000000000000000000 ) ) ;
#3524=ORIENTED_EDGE ( 'NONE', *, *, #1, .F. ) ;
#3531=ORIENTED_EDGE ( 'NONE', *, *, #1977, .F. ) ;
#3538=DIRECTION ( 'NONE',  ( 0.000000000000000000, -0.000000000000000000, 1.000000000000000000 ) ) ;
#3539=ORIENTED_EDGE ( 'NONE', *, *, #3708, .F. ) ;
#3548=ADVANCED_FACE ( 'NONE', ( #3113 ), #15, .T. ) ;
#3559=ORIENTED_EDGE ( 'NONE', *, *, #5549, .F. ) ;
#3560=B_SPLINE_CURVE_WITH_KNOTS ( 'NONE', 3,
 ( #84, #3742, #4395, #1415, #713, #3814, #1982, #2067, #4558, #5710, #1248, #1372, #6244, #2599, #3084, #5624, #634, #5127, #7590, #3132, #4514, #5006, #2518, #3857, #6940, #6326, #7549, #122, #1943, #6902, #3892, #1290, #5091, #5660, #3208, #3780, #6284, #4432, #2640, #6369, #755, #668, #792, #7629, #3165, #7713, #1326, #38, #2559, #7667, #5049, #3291, #4470, #6983, #5789, #3248, #5753, #2020, #7030, #6411, #168 ),
 .UNSPECIFIED., .F., .F.,
 ( 4, 2, 2, 2, 2, 2, 2, 2, 2, 2, 2, 1, 2, 2, 2, 2, 2, 2, 2, 2, 2, 2, 2, 2, 2, 2, 2, 2, 2, 2, 4 ),
 ( 0.1042068716910059117, 0.1107198011716938740, 0.1139762659120378552, 0.1172327306523818502, 0.1237456601330697986, 0.1253738925032417961, 0.1270021248734137798, 0.1302585896137577470, 0.1367715190944456816, 0.1383997514646176930, 0.1400279838347896766, 0.1432844485751335883, 0.1465409133154775279, 0.1481691456856495115, 0.1497973780558214951, 0.1563103075365094574, 0.1595667722768534524, 0.1611950046470254361, 0.1628232370171974197, 0.1693361664978854098, 0.1709643988680573656, 0.1725926312382293215, 0.1758490959785732333, 0.1823620254592609458, 0.1856184901996048298, 0.1888749549399486583, 0.1921314196802925145, 0.1953878844206363707, 0.2019008139013241110, 0.2051572786416679672, 0.2084137433820118235 ),
 .UNSPECIFIED. ) ;
#3561=CARTESIAN_POINT ( 'NONE',  ( 0.000000000000000000, 5.151388682096968097, -2.749999999536767437 ) ) ;
#3564=CARTESIAN_POINT ( 'NONE',  ( 1.312500000184909199, 4.908106857043937232, 3.316250000000001030 ) ) ;
#3572=LINE ( 'NONE', #4018, #309 ) ;
#3575=DIRECTION ( 'NONE',  ( -1.000000000000000000, -0.000000000000000000, -0.000000000000000000 ) ) ;
#3580=ORIENTED_EDGE ( 'NONE', *, *, #6831, .F. ) ;
#3582=EDGE_CURVE ( 'NONE', #2355, #6986, #733, .T. ) ;
#3585=CARTESIAN_POINT ( 'NONE',  ( 0.000000000000000000, 1.750000000000000666, -3.343750000000000444 ) ) ;
#3586=DIRECTION ( 'NONE',  ( -0.000000000000000000, 0.000000000000000000, 1.000000000000000000 ) ) ;
#3591=VECTOR ( 'NONE', #6028, 39.37007874015748143 ) ;
#3593=CARTESIAN_POINT ( 'NONE',  ( 1.312500000000000222, 7.964000000000000412, 2.411250000000000338 ) ) ;
#3597=DIRECTION ( 'NONE',  ( -0.000000000000000000, -0.000000000000000000, 1.000000000000000000 ) ) ;
#3616=ORIENTED_EDGE ( 'NONE', *, *, #5286, .T. ) ;
#3620=VERTEX_POINT ( 'NONE', #2501 ) ;
#3622=VECTOR ( 'NONE', #4584, 39.37007874015748143 ) ;
#3624=EDGE_LOOP ( 'NONE', ( #6120, #4219, #4402, #6052, #6346, #5583 ) ) ;
#3627=VERTEX_POINT ( 'NONE', #7569 ) ;
#3630=DIRECTION ( 'NONE',  ( -0.000000000000000000, -0.000000000000000000, 1.000000000000000000 ) ) ;
#3631=CARTESIAN_POINT ( 'NONE',  ( 0.6696957874015749823, 2.330452401574803822, -5.651700944881890010 ) ) ;
#3632=CARTESIAN_POINT ( 'NONE',  ( 2.750000000000000444, 7.964000000000000412, 3.691250000000001030 ) ) ;
#3639=EDGE_CURVE ( 'NONE', #2678, #7297, #838, .T. ) ;
#3642=ORIENTED_EDGE ( 'NONE', *, *, #1193, .T. ) ;
#3646=CARTESIAN_POINT ( 'NONE',  ( -0.5808953455350218675, 5.130091789537773117, -5.108750000000001457 ) ) ;
#3651=CARTESIAN_POINT ( 'NONE',  ( -2.750000000000000444, 7.964000000000000412, 3.691250000000001030 ) ) ;
#3652=ORIENTED_EDGE ( 'NONE', *, *, #4375, .F. ) ;
#3657=EDGE_CURVE ( 'NONE', #4253, #7385, #1702, .T. ) ;
#3658=ORIENTED_EDGE ( 'NONE', *, *, #4476, .T. ) ;
#3666=DIRECTION ( 'NONE',  ( -0.000000000000000000, -1.000000000000000000, 0.000000000000000000 ) ) ;
#3670=CARTESIAN_POINT ( 'NONE',  ( -2.750000000000000444, 7.521783346446682117, 3.691250000461920866 ) ) ;
#3675=CYLINDRICAL_SURFACE ( 'NONE', #2189, 1.624999999999999778 ) ;
#3682=ADVANCED_FACE ( 'NONE', ( #5963, #1086 ), #343, .T. ) ;
#3684=FACE_OUTER_BOUND ( 'NONE', #6309, .T. ) ;
#3693=EDGE_LOOP ( 'NONE', ( #7436, #3197, #8152, #4417, #4117, #573 ) ) ;
#3695=FACE_BOUND ( 'NONE', #8103, .T. ) ;
#3697=ORIENTED_EDGE ( 'NONE', *, *, #3163, .F. ) ;
#3698=ORIENTED_EDGE ( 'NONE', *, *, #1192, .F. ) ;
#3700=CARTESIAN_POINT ( 'NONE',  ( 3.179822820131703587, 2.000074507168632554, -0.5625000000000001110 ) ) ;
#3703=VERTEX_POINT ( 'NONE', #8021 ) ;
#3706=VECTOR ( 'NONE', #4624, 39.37007874015748143 ) ;
#3708=EDGE_CURVE ( 'NONE', #3004, #2473, #2358, .T. ) ;
#3709=VECTOR ( 'NONE', #1011, 39.37007874015748143 ) ;
#3710=CIRCLE ( 'NONE', #176, 0.2625000000000008438 ) ;
#3731=B_SPLINE_CURVE_WITH_KNOTS ( 'NONE', 3,
 ( #8168, #5637, #139, #99, #4451, #1340 ),
 .UNSPECIFIED., .F., .F.,
 ( 4, 2, 4 ),
 ( 2.166691104215167967E-12, 0.007631658729071641098, 0.01526331745597659002 ),
 .UNSPECIFIED. ) ;
#3732=EDGE_CURVE ( 'NONE', #2439, #3378, #7107, .T. ) ;
#3734=DIRECTION ( 'NONE',  ( 0.000000000000000000, 0.000000000000000000, 1.000000000000000000 ) ) ;
#3736=CARTESIAN_POINT ( 'NONE',  ( 0.000000000000000000, 0.000000000000000000, 0.000000000000000000 ) ) ;
#3737=VECTOR ( 'NONE', #4433, 39.37007874015748143 ) ;
#3738=EDGE_LOOP ( 'NONE', ( #1783, #4605, #1029, #1413 ) ) ;
#3741=CARTESIAN_POINT ( 'NONE',  ( 2.946793809113656959, 2.499999999120089189, 0.5624999991014997258 ) ) ;
#3742=CARTESIAN_POINT ( 'NONE',  ( 0.08551594028232864519, 2.637422184226597022, -5.108750000000001457 ) ) ;
#3744=EDGE_LOOP ( 'NONE', ( #7307, #1649, #1736, #5867 ) ) ;
#3749=EDGE_CURVE ( 'NONE', #4674, #1923, #3452, .T. ) ;
#3753=CARTESIAN_POINT ( 'NONE',  ( 0.000000000000000000, 7.964000000000000412, 0.000000000000000000 ) ) ;
#3754=CARTESIAN_POINT ( 'NONE',  ( -2.750000000000000444, 7.521783346446679452, 3.691250000461920422 ) ) ;
#3756=ORIENTED_EDGE ( 'NONE', *, *, #830, .F. ) ;
#3761=FACE_OUTER_BOUND ( 'NONE', #1313, .T. ) ;
#3774=FACE_OUTER_BOUND ( 'NONE', #4202, .T. ) ;
#3778=EDGE_CURVE ( 'NONE', #4596, #6749, #8093, .T. ) ;
#3780=CARTESIAN_POINT ( 'NONE',  ( 1.291725143358333661, 4.183586393851094876, -5.108749999999998792 ) ) ;
#3784=CARTESIAN_POINT ( 'NONE',  ( 0.000000000000000000, 5.339000000000000412, 0.1249999999999997641 ) ) ;
#3785=VERTEX_POINT ( 'NONE', #3741 ) ;
#3786=DIRECTION ( 'NONE',  ( 0.000000000000000000, -0.000000000000000000, 1.000000000000000000 ) ) ;
#3787=DIRECTION ( 'NONE',  ( -1.000000000000000000, -0.000000000000000000, 0.000000000000000000 ) ) ;
#3797=DIRECTION ( 'NONE',  ( 0.000000000000000000, 0.000000000000000000, -1.000000000000000000 ) ) ;
#3808=LINE ( 'NONE', #1320, #6345 ) ;
#3811=ORIENTED_EDGE ( 'NONE', *, *, #78, .T. ) ;
#3814=CARTESIAN_POINT ( 'NONE',  ( 0.4206575512004037121, 2.705990808344437948, -5.108749999999997904 ) ) ;
#3816=ORIENTED_EDGE ( 'NONE', *, *, #7093, .F. ) ;
#3818=ORIENTED_EDGE ( 'NONE', *, *, #2536, .T. ) ;
#3819=EDGE_CURVE ( 'NONE', #3476, #5226, #7508, .T. ) ;
#3820=EDGE_CURVE ( 'NONE', #2183, #7868, #6162, .T. ) ;
#3821=CARTESIAN_POINT ( 'NONE',  ( -0.001186137648316157355, 2.637500537863615158, -5.108750000000001457 ) ) ;
#3823=DIRECTION ( 'NONE',  ( 1.000000000000000000, 0.000000000000000000, 0.000000000000000000 ) ) ;
#3824=EDGE_LOOP ( 'NONE', ( #1789, #5997, #6844, #5437 ) ) ;
#3827=FACE_OUTER_BOUND ( 'NONE', #1234, .T. ) ;
#3830=CARTESIAN_POINT ( 'NONE',  ( -2.537500000000000533, 1.664000000000000368, 0.000000000000000000 ) ) ;
#3833=EDGE_CURVE ( 'NONE', #540, #7519, #4652, .T. ) ;
#3834=DIRECTION ( 'NONE',  ( -0.000000000000000000, -1.000000000000000000, 0.000000000000000000 ) ) ;
#3835=DIRECTION ( 'NONE',  ( 0.000000000000000000, -1.000000000000000000, 0.000000000000000000 ) ) ;
#3837=CARTESIAN_POINT ( 'NONE',  ( 0.000000000000000000, 7.521783347225603045, 3.691250000923840258 ) ) ;
#3841=AXIS2_PLACEMENT_3D ( 'NONE', #2319, #5588, #4227 ) ;
#3843=ORIENTED_EDGE ( 'NONE', *, *, #3778, .T. ) ;
#3844=VECTOR ( 'NONE', #3434, 39.37007874015748143 ) ;
#3847=DIRECTION ( 'NONE',  ( 0.000000000000000000, 0.000000000000000000, 1.000000000000000000 ) ) ;
#3848=DIRECTION ( 'NONE',  ( -0.000000000000000000, 1.000000000000000000, 0.000000000000000000 ) ) ;
#3851=AXIS2_PLACEMENT_3D ( 'NONE', #6572, #2246, #5312 ) ;
#3855=CONICAL_SURFACE ( 'NONE', #3483, 3.343750000098590913, 0.4297622790966889594 ) ;
#3856=PRODUCT_DEFINITION ( 'UNKNOWN', '', #2206, #4800 ) ;
#3857=CARTESIAN_POINT ( 'NONE',  ( 1.242854517407008030, 3.525957823492111398, -5.108750000000003233 ) ) ;
#3863=DIRECTION ( 'NONE',  ( -0.000000000000000000, -0.000000000000000000, 1.000000000000000000 ) ) ;
#3864=CARTESIAN_POINT ( 'NONE',  ( -1.625000000000000222, 5.113999999999999879, -2.750000000000000444 ) ) ;
#3865=AXIS2_PLACEMENT_3D ( 'NONE', #564, #5640, #2541 ) ;
#3869=FACE_OUTER_BOUND ( 'NONE', #1755, .T. ) ;
#3871=VECTOR ( 'NONE', #523, 39.37007874015748143 ) ;
#3875=EDGE_CURVE ( 'NONE', #3252, #4495, #4225, .T. ) ;
#3882=VERTEX_POINT ( 'NONE', #6818 ) ;
#3883=CARTESIAN_POINT ( 'NONE',  ( 1.624999999999999778, 3.950000000000000178, -5.108750000000001457 ) ) ;
#3884=DIRECTION ( 'NONE',  ( -1.000000000000000000, 0.000000000000000000, 0.000000000000000000 ) ) ;
#3888=EDGE_CURVE ( 'NONE', #47, #7868, #5622, .T. ) ;
#3889=UNCERTAINTY_MEASURE_WITH_UNIT (LENGTH_MEASURE( 1.000000000000000082E-05 ), #908, 'distance_accuracy_value', 'NONE');
#3892=CARTESIAN_POINT ( 'NONE',  ( 1.312565956928763322, 3.990720461577614842, -5.108749999999999680 ) ) ;
#3894=PLANE ( 'NONE',  #5055 ) ;
#3904=CARTESIAN_POINT ( 'NONE',  ( -1.274606804493992884, 2.434036455850696168, -2.750000000000000444 ) ) ;
#3909=DIRECTION ( 'NONE',  ( -1.000000000000000000, -0.000000000000000000, 0.000000000000000000 ) ) ;
#3921=EDGE_CURVE ( 'NONE', #5733, #277, #3710, .T. ) ;
#3925=ORIENTED_EDGE ( 'NONE', *, *, #6520, .F. ) ;
#3935=FACE_OUTER_BOUND ( 'NONE', #1308, .T. ) ;
#3941=CARTESIAN_POINT ( 'NONE',  ( -1.198957880828181333, 2.500000000000000000, -2.750000000000000444 ) ) ;
#3942=ORIENTED_EDGE ( 'NONE', *, *, #2647, .T. ) ;
#3946=ORIENTED_EDGE ( 'NONE', *, *, #3921, .F. ) ;
#3953=ORIENTED_EDGE ( 'NONE', *, *, #19, .T. ) ;
#3958=CARTESIAN_POINT ( 'NONE',  ( -1.177243217050785162, 4.531893234618878274, -5.108749999999998792 ) ) ;
#3964=VECTOR ( 'NONE', #7150, 39.37007874015748143 ) ;
#3966=CARTESIAN_POINT ( 'NONE',  ( 0.7335700393700786970, 2.500000000000000444, -0.5625000000000003331 ) ) ;
#3968=ORIENTED_EDGE ( 'NONE', *, *, #5516, .T. ) ;
#3970=ORIENTED_EDGE ( 'NONE', *, *, #8011, .T. ) ;
#3972=EDGE_CURVE ( 'NONE', #8146, #7577, #5013, .T. ) ;
#3975=CARTESIAN_POINT ( 'NONE',  ( 0.000000000000000000, 3.950000000000000178, -2.750000000000000444 ) ) ;
#3978=ADVANCED_FACE ( 'NONE', ( #7922 ), #2225, .T. ) ;
#3985=DIRECTION ( 'NONE',  ( -1.000000000000000000, -0.000000000000000000, 0.000000000000000000 ) ) ;
#3989=CARTESIAN_POINT ( 'NONE',  ( -1.625000000000000222, 5.339000000000000412, 0.1249999999999997641 ) ) ;
#3993=AXIS2_PLACEMENT_3D ( 'NONE', #264, #756, #6370 ) ;
#3995=DIRECTION ( 'NONE',  ( 0.000000000000000000, 0.000000000000000000, 1.000000000000000000 ) ) ;
#3998=AXIS2_PLACEMENT_3D ( 'NONE', #2121, #7647, #3797 ) ;
#4001=ORIENTED_EDGE ( 'NONE', *, *, #2396, .F. ) ;
#4002=PLANE ( 'NONE',  #4637 ) ;
#4005=DIRECTION ( 'NONE',  ( 1.000000000000000000, 0.000000000000000000, -0.000000000000000000 ) ) ;
#4010=CARTESIAN_POINT ( 'NONE',  ( -1.102289202651617339, 4.662797418998615662, -5.108749999999997904 ) ) ;
#4011=DIRECTION ( 'NONE',  ( 0.000000000000000000, -0.000000000000000000, 1.000000000000000000 ) ) ;
#4018=CARTESIAN_POINT ( 'NONE',  ( 2.750000000000000444, 8.601289606299213020, 3.323749999933555355 ) ) ;
#4028=ORIENTED_EDGE ( 'NONE', *, *, #6889, .F. ) ;
#4030=CARTESIAN_POINT ( 'NONE',  ( 1.625000000000000222, 0.000000000000000000, 0.1249999999999997641 ) ) ;
#4034=DIRECTION ( 'NONE',  ( 1.000000000000000000, 0.000000000000000000, 0.000000000000000000 ) ) ;
#4039=ORIENTED_EDGE ( 'NONE', *, *, #5942, .F. ) ;
#4040=EDGE_CURVE ( 'NONE', #1998, #7338, #1002, .T. ) ;
#4044=CARTESIAN_POINT ( 'NONE',  ( -1.267418543289768884, 4.291720194162276236, -5.108750000000002345 ) ) ;
#4047=CARTESIAN_POINT ( 'NONE',  ( 1.625000000000000222, 5.639000000000001123, -2.750000000000000444 ) ) ;
#4049=EDGE_LOOP ( 'NONE', ( #7143, #2835, #7903, #6182 ) ) ;
#4059=ORIENTED_EDGE ( 'NONE', *, *, #1606, .F. ) ;
#4060=CARTESIAN_POINT ( 'NONE',  ( -1.625000000000000222, 5.339000000000000412, 0.1250000000000000278 ) ) ;
#4067=DIRECTION ( 'NONE',  ( -0.000000000000000000, 1.000000000000000000, -0.000000000000000000 ) ) ;
#4069=ORIENTED_EDGE ( 'NONE', *, *, #3875, .T. ) ;
#4071=ORIENTED_EDGE ( 'NONE', *, *, #882, .T. ) ;
#4072=FACE_OUTER_BOUND ( 'NONE', #3744, .T. ) ;
#4079=EDGE_CURVE ( 'NONE', #1059, #6055, #3572, .T. ) ;
#4081=CARTESIAN_POINT ( 'NONE',  ( -1.270916235774476322, 3.611191510761752710, -5.108749999999999680 ) ) ;
#4082=CARTESIAN_POINT ( 'NONE',  ( 0.4460230445270007560, 2.387088541186376922, 3.019143986898724652 ) ) ;
#4083=CARTESIAN_POINT ( 'NONE',  ( 2.750000000000000444, 7.964000000000000412, 3.323750000000001759 ) ) ;
#4093=LINE ( 'NONE', #1003, #4887 ) ;
#4097=AXIS2_PLACEMENT_3D ( 'NONE', #77, #6492, #1975 ) ;
#4102=DIRECTION ( 'NONE',  ( -1.000000000000000000, 0.000000000000000000, -0.000000000000000000 ) ) ;
#4111=AXIS2_PLACEMENT_3D ( 'NONE', #2726, #5213, #6378 ) ;
#4113=ORIENTED_EDGE ( 'NONE', *, *, #7197, .F. ) ;
#4115=ORIENTED_EDGE ( 'NONE', *, *, #7725, .F. ) ;
#4117=ORIENTED_EDGE ( 'NONE', *, *, #6953, .F. ) ;
#4120=CARTESIAN_POINT ( 'NONE',  ( -1.625000000000000222, 0.000000000000000000, 0.000000000000000000 ) ) ;
#4121=ADVANCED_FACE ( 'NONE', ( #4677, #421 ), #7191, .T. ) ;
#4124=CARTESIAN_POINT ( 'NONE',  ( -1.625000000000000222, 2.359134605239151750, 2.598586947464774255 ) ) ;
#4127=FACE_BOUND ( 'NONE', #5483, .T. ) ;
#4128=DIRECTION ( 'NONE',  ( 0.000000000000000000, 0.000000000000000000, -1.000000000000000000 ) ) ;
#4132=ORIENTED_EDGE ( 'NONE', *, *, #2807, .T. ) ;
#4133=CARTESIAN_POINT ( 'NONE',  ( 0.000000000000000000, 5.339000000000000412, -2.750000000000000444 ) ) ;
#4136=CIRCLE ( 'NONE', #1279, 1.624999999999999778 ) ;
#4151=CARTESIAN_POINT ( 'NONE',  ( 1.312500000000000444, 8.589000000000000412, 2.411250000000000782 ) ) ;
#4157=ORIENTED_EDGE ( 'NONE', *, *, #4079, .T. ) ;
#4166=CARTESIAN_POINT ( 'NONE',  ( -0.2278558862525867923, 2.340729989832576852, 3.064709232292516017 ) ) ;
#4179=VERTEX_POINT ( 'NONE', #1236 ) ;
#4181=EDGE_LOOP ( 'NONE', ( #1409, #7786, #7155, #3287 ) ) ;
#4186=LINE ( 'NONE', #1087, #3172 ) ;
#4187=DIRECTION ( 'NONE',  ( 0.000000000000000000, 0.000000000000000000, -1.000000000000000000 ) ) ;
#4194=ORIENTED_EDGE ( 'NONE', *, *, #1642, .T. ) ;
#4195=CARTESIAN_POINT ( 'NONE',  ( 1.625000000000000222, 5.339000000000000412, -2.750000000000000444 ) ) ;
#4202=EDGE_LOOP ( 'NONE', ( #4039, #5861, #2723, #3272, #2595, #7115, #4808, #1596 ) ) ;
#4218=EDGE_CURVE ( 'NONE', #417, #1507, #4843, .T. ) ;
#4219=ORIENTED_EDGE ( 'NONE', *, *, #2684, .F. ) ;
#4220=ADVANCED_FACE ( 'NONE', ( #2957 ), #7539, .F. ) ;
#4221=ADVANCED_FACE ( 'NONE', ( #4878 ), #1283, .F. ) ;
#4223=AXIS2_PLACEMENT_3D ( 'NONE', #3975, #5709, #83 ) ;
#4224=EDGE_CURVE ( 'NONE', #3882, #7586, #7367, .T. ) ;
#4225=LINE ( 'NONE', #3131, #7407 ) ;
#4226=CARTESIAN_POINT ( 'NONE',  ( -3.343750000000001776, 1.750000000000000444, -0.5625000000000003331 ) ) ;
#4227=DIRECTION ( 'NONE',  ( 0.000000000000000000, 0.000000000000000000, -1.000000000000000000 ) ) ;
#4232=VECTOR ( 'NONE', #4743, 39.37007874015748143 ) ;
#4233=CARTESIAN_POINT ( 'NONE',  ( -1.500000000000000444, 5.339000000000000412, 0.1249999999999999445 ) ) ;
#4235=EDGE_CURVE ( 'NONE', #3703, #5265, #8147, .T. ) ;
#4237=VECTOR ( 'NONE', #5650, 39.37007874015748143 ) ;
#4243=DIRECTION ( 'NONE',  ( 0.000000000000000000, 0.000000000000000000, -1.000000000000000000 ) ) ;
#4244=CIRCLE ( 'NONE', #2683, 2.999999999940156759 ) ;
#4245=CARTESIAN_POINT ( 'NONE',  ( -0.4616491105740681000, 5.179384528936357590, -5.108750000000002345 ) ) ;
#4249=PRODUCT_DEFINITION_SHAPE ( 'NONE', 'NONE',  #3856 ) ;
#4253=VERTEX_POINT ( 'NONE', #461 ) ;
#4257=CARTESIAN_POINT ( 'NONE',  ( -1.625000000000000222, 2.057992047244095346, -2.750000000000000444 ) ) ;
#4264=VECTOR ( 'NONE', #2974, 39.37007874015748143 ) ;
#4268=DIRECTION ( 'NONE',  ( -1.000000000000000000, 0.000000000000000000, -0.000000000000000000 ) ) ;
#4274=VECTOR ( 'NONE', #409, 39.37007874015748143 ) ;
#4275=CARTESIAN_POINT ( 'NONE',  ( 0.000000000000000000, 2.325000000000000622, -3.080208333333334103 ) ) ;
#4284=DIMENSIONAL_EXPONENTS ( 1.000000000000000000, 0.000000000000000000, 0.000000000000000000, 0.000000000000000000, 0.000000000000000000, 0.000000000000000000, 0.000000000000000000 ) ;
#4292=CARTESIAN_POINT ( 'NONE',  ( -0.6563132439730009482, 5.089852872402901518, -5.108749999999999680 ) ) ;
#4295=CARTESIAN_POINT ( 'NONE',  ( 1.625000000000000222, 5.113999999999999879, 2.750000000234376074 ) ) ;
#4297=LINE ( 'NONE', #6838, #5797 ) ;
#4298=VERTEX_POINT ( 'NONE', #5578 ) ;
#4304=VERTEX_POINT ( 'NONE', #8142 ) ;
#4306=ORIENTED_EDGE ( 'NONE', *, *, #7527, .T. ) ;
#4307=LINE ( 'NONE', #2306, #5259 ) ;
#4312=DIRECTION ( 'NONE',  ( -1.000000000000000000, -0.000000000000000000, 0.000000000000000000 ) ) ;
#4314=CARTESIAN_POINT ( 'NONE',  ( 1.504804212598425783, 5.036377244094489392, -5.293879055118110522 ) ) ;
#4321=ADVANCED_FACE ( 'NONE', ( #1848 ), #2511, .F. ) ;
#4325=ORIENTED_EDGE ( 'NONE', *, *, #882, .F. ) ;
#4331=( BOUNDED_CURVE ( )  B_SPLINE_CURVE ( 2, ( #5341, #3473, #979, #4957, #2625, #2003, #6343, #4986, #5727 ),
 .UNSPECIFIED., .F., .F. ) 
 B_SPLINE_CURVE_WITH_KNOTS ( ( 3, 2, 2, 2, 3 ),
 ( 1.235375695993373051E-14, 0.004098851372437040987, 0.03173539256035051714, 0.05937193374826417458, 0.07317982560813471316 ),
 .UNSPECIFIED. ) 
 CURVE ( )  GEOMETRIC_REPRESENTATION_ITEM ( )  RATIONAL_B_SPLINE_CURVE ( ( 0.9260057553135151442, 0.9565602018087399072, 1.000000000000000000, 0.7071067811865479058, 1.000000000000000000, 0.7071067811865479058, 1.000000000000000000, 0.8536633850130518342, 0.8535534732088589926 ) ) 
 REPRESENTATION_ITEM ( '' )  );
#4336=DIRECTION ( 'NONE',  ( -0.000000000000000000, -1.000000000000000000, 0.000000000000000000 ) ) ;
#4338=ORIENTED_EDGE ( 'NONE', *, *, #6890, .T. ) ;
#4341=CARTESIAN_POINT ( 'NONE',  ( 0.000000000000000000, 5.151388682096968097, 2.749999999536767437 ) ) ;
#4346=EDGE_CURVE ( 'NONE', #1721, #7577, #4505, .T. ) ;
#4351=ORIENTED_EDGE ( 'NONE', *, *, #7634, .F. ) ;
#4353=DIRECTION ( 'NONE',  ( 0.000000000000000000, 0.000000000000000000, -1.000000000000000000 ) ) ;
#4354=VECTOR ( 'NONE', #4268, 39.37007874015748143 ) ;
#4359=CARTESIAN_POINT ( 'NONE',  ( -0.1312789392238629671, 2.329012898157790001, -3.076250280708381801 ) ) ;
#4362=AXIS2_PLACEMENT_3D ( 'NONE', #3561, #6064, #450 ) ;
#4369=CARTESIAN_POINT ( 'NONE',  ( 3.063407153363070012, 2.250083286129449966, 0.5624999982029994516 ) ) ;
#4371=VECTOR ( 'NONE', #5944, 39.37007874015748143 ) ;
#4375=EDGE_CURVE ( 'NONE', #674, #1793, #5779, .T. ) ;
#4377=VERTEX_POINT ( 'NONE', #7018 ) ;
#4378=CARTESIAN_POINT ( 'NONE',  ( -1.625000000000000222, 2.500000000000000000, 2.521780125229002412 ) ) ;
#4382=ADVANCED_FACE ( 'NONE', ( #3774 ), #1405, .T. ) ;
#4387=EDGE_CURVE ( 'NONE', #7338, #6439, #2278, .T. ) ;
#4394=DIRECTION ( 'NONE',  ( 1.000000000000000000, 0.000000000000000000, 0.000000000000000000 ) ) ;
#4395=CARTESIAN_POINT ( 'NONE',  ( 0.1707770588212104701, 2.645851873985466174, -5.108749999999999680 ) ) ;
#4397=VERTEX_POINT ( 'NONE', #5159 ) ;
#4399=LINE ( 'NONE', #3784, #2314 ) ;
#4401=CIRCLE ( 'NONE', #7156, 1.624999999999999778 ) ;
#4402=ORIENTED_EDGE ( 'NONE', *, *, #8011, .F. ) ;
#4403=APPLICATION_CONTEXT ( 'configuration controlled 3d designs of mechanical parts and assemblies' ) ;
#4406=CARTESIAN_POINT ( 'NONE',  ( 0.7335700378700447111, 2.500000000079424911, -2.749999999768383940 ) ) ;
#4414=CARTESIAN_POINT ( 'NONE',  ( -3.063407152776790543, 2.250083286516130432, 0.5624999999177930921 ) ) ;
#4415=CARTESIAN_POINT ( 'NONE',  ( -1.625000000000000222, 2.500000000077463369, -2.521780125186765975 ) ) ;
#4417=ORIENTED_EDGE ( 'NONE', *, *, #7910, .F. ) ;
#4422=ORIENTED_EDGE ( 'NONE', *, *, #7093, .T. ) ;
#4425=DIRECTION ( 'NONE',  ( -1.000000000000000000, -0.000000000000000000, -0.000000000000000000 ) ) ;
#4428=DIRECTION ( 'NONE',  ( 0.000000000000000000, 0.000000000000000000, 1.000000000000000000 ) ) ;
#4430=ORIENTED_EDGE ( 'NONE', *, *, #3639, .F. ) ;
#4432=CARTESIAN_POINT ( 'NONE',  ( 1.246236519039154444, 4.370643088443840085, -5.108749999999997904 ) ) ;
#4433=DIRECTION ( 'NONE',  ( -1.000000000000000000, -0.000000000000000000, 0.000000000000000000 ) ) ;
#4434=ORIENTED_EDGE ( 'NONE', *, *, #8133, .F. ) ;
#4435=CARTESIAN_POINT ( 'NONE',  ( 1.625000000000000222, 0.000000000000000000, 0.000000000000000000 ) ) ;
#4440=LINE ( 'NONE', #6556, #7151 ) ;
#4442=DIRECTION ( 'NONE',  ( -0.000000000000000000, -0.000000000000000000, 1.000000000000000000 ) ) ;
#4443=B_SPLINE_CURVE_WITH_KNOTS ( 'NONE', 3,
 ( #304, #4764, #4723, #5335, #1544, #7803 ),
 .UNSPECIFIED., .F., .F.,
 ( 4, 2, 4 ),
 ( 9.813077866773594792E-18, 0.007631658735546109629, 0.01526331747109221058 ),
 .UNSPECIFIED. ) ;
#4451=CARTESIAN_POINT ( 'NONE',  ( -1.557862129473126966, 2.150738729911186198, 2.750000000000000444 ) ) ;
#4461=DIRECTION ( 'NONE',  ( 0.000000000000000000, 0.000000000000000000, -1.000000000000000000 ) ) ;
#4463=CARTESIAN_POINT ( 'NONE',  ( -2.537500000000000533, 2.500000000000000444, -0.000000000000000000 ) ) ;
#4466=ORIENTED_EDGE ( 'NONE', *, *, #4851, .F. ) ;
#4467=ORIENTED_EDGE ( 'NONE', *, *, #1077, .F. ) ;
#4470=CARTESIAN_POINT ( 'NONE',  ( 0.5830436418431348411, 5.126677097923686865, -5.108750000000001457 ) ) ;
#4476=EDGE_CURVE ( 'NONE', #277, #5733, #710, .T. ) ;
#4477=LINE ( 'NONE', #6462, #3339 ) ;
#4486=DIRECTION ( 'NONE',  ( 1.000000000000000000, 0.000000000000000000, 0.000000000000000000 ) ) ;
#4491=VERTEX_POINT ( 'NONE', #818 ) ;
#4493=DIRECTION ( 'NONE',  ( 1.000000000000000000, 0.000000000000000000, -0.000000000000000000 ) ) ;
#4495=VERTEX_POINT ( 'NONE', #5199 ) ;
#4497=EDGE_CURVE ( 'NONE', #445, #6962, #7745, .T. ) ;
#4503=AXIS2_PLACEMENT_3D ( 'NONE', #1528, #5276, #4011 ) ;
#4504=CARTESIAN_POINT ( 'NONE',  ( -1.201750196850394081, 2.500000000000000444, 2.750000000000000444 ) ) ;
#4505=LINE ( 'NONE', #3883, #454 ) ;
#4513=CONICAL_SURFACE ( 'NONE', #205, 3.343750000040417447, 0.4297622790966887374 ) ;
#4514=CARTESIAN_POINT ( 'NONE',  ( 1.146819099299166034, 3.311311129500751793, -5.108750000000002345 ) ) ;
#4515=CARTESIAN_POINT ( 'NONE',  ( 0.6237442712837091285, 2.448197894244100947, -2.959338728480837233 ) ) ;
#4520=CARTESIAN_POINT ( 'NONE',  ( 1.489119986973711507, 2.223645902782970030, 2.749999999536767437 ) ) ;
#4523=CARTESIAN_POINT ( 'NONE',  ( -3.343750000000002220, 2.500000000000000444, -0.5624999994010003723 ) ) ;
#4526=VECTOR ( 'NONE', #2328, 39.37007874015748143 ) ;
#4539=DIRECTION ( 'NONE',  ( 0.000000000000000000, 0.000000000000000000, 1.000000000000000000 ) ) ;
#4549=EDGE_CURVE ( 'NONE', #3004, #3267, #2252, .T. ) ;
#4552=B_SPLINE_CURVE_WITH_KNOTS ( 'NONE', 3,
 ( #8162, #1865, #4980, #553 ),
 .UNSPECIFIED., .F., .F.,
 ( 4, 4 ),
 ( 1.026013551136062230E-11, 0.01222568458709676585 ),
 .UNSPECIFIED. ) ;
#4554=ORIENTED_EDGE ( 'NONE', *, *, #7921, .F. ) ;
#4558=CARTESIAN_POINT ( 'NONE',  ( 0.6563132712551269510, 2.810147165011805725, -5.108750000000004121 ) ) ;
#4559=CARTESIAN_POINT ( 'NONE',  ( 2.946793808523474834, 2.500000000017352786, -0.5625000000000002220 ) ) ;
#4566=CARTESIAN_POINT ( 'NONE',  ( 0.000000000000000000, 3.950000000000000178, -5.108750000000001457 ) ) ;
#4576=ORIENTED_EDGE ( 'NONE', *, *, #2407, .T. ) ;
#4578=ORIENTED_EDGE ( 'NONE', *, *, #730, .F. ) ;
#4579=CARTESIAN_POINT ( 'NONE',  ( -1.500000000000000444, 3.950000000000000178, 2.749999998413802160 ) ) ;
#4584=DIRECTION ( 'NONE',  ( -0.000000000000000000, -0.000000000000000000, 1.000000000000000000 ) ) ;
#4586=ORIENTED_EDGE ( 'NONE', *, *, #2367, .F. ) ;
#4589=EDGE_CURVE ( 'NONE', #2473, #5196, #3444, .T. ) ;
#4590=CARTESIAN_POINT ( 'NONE',  ( -1.146819095829421098, 4.588688891394698821, -5.108749999999999680 ) ) ;
#4593=LINE ( 'NONE', #3966, #7133 ) ;
#4596=VERTEX_POINT ( 'NONE', #253 ) ;
#4604=DIRECTION ( 'NONE',  ( 1.000000000000000000, 0.000000000000000000, -0.000000000000000000 ) ) ;
#4605=ORIENTED_EDGE ( 'NONE', *, *, #1980, .T. ) ;
#4611=LINE ( 'NONE', #6522, #2964 ) ;
#4615=LINE ( 'NONE', #4734, #3844 ) ;
#4619=CARTESIAN_POINT ( 'NONE',  ( -0.7335700378053525705, 2.500000000126119559, -5.108750000000001457 ) ) ;
#4624=DIRECTION ( 'NONE',  ( 0.000000000000000000, 1.000000000000000000, 0.000000000000000000 ) ) ;
#4625=EDGE_CURVE ( 'NONE', #5748, #6859, #5992, .T. ) ;
#4626=CIRCLE ( 'NONE', #8096, 1.624999995942718156 ) ;
#4627=PLANE ( 'NONE',  #4503 ) ;
#4628=AXIS2_PLACEMENT_3D ( 'NONE', #290, #4128, #2748 ) ;
#4634=EDGE_CURVE ( 'NONE', #5899, #2392, #2871, .T. ) ;
#4637=AXIS2_PLACEMENT_3D ( 'NONE', #2740, #7904, #4697 ) ;
#4641=EDGE_CURVE ( 'NONE', #4731, #4304, #5358, .T. ) ;
#4643=ORIENTED_EDGE ( 'NONE', *, *, #6970, .F. ) ;
#4652=B_SPLINE_CURVE_WITH_KNOTS ( 'NONE', 3,
 ( #6125, #3037, #3700, #1822 ),
 .UNSPECIFIED., .F., .F.,
 ( 4, 4 ),
 ( 4.860009891584967381E-13, 0.02101476597452160006 ),
 .UNSPECIFIED. ) ;
#4654=FACE_OUTER_BOUND ( 'NONE', #5543, .T. ) ;
#4661=EDGE_CURVE ( 'NONE', #1998, #2981, #2016, .T. ) ;
#4667=CARTESIAN_POINT ( 'NONE',  ( -1.113928750309983506, 4.644468174584341469, -5.108750000000003233 ) ) ;
#4668=CARTESIAN_POINT ( 'NONE',  ( -0.4482830794785033768, 2.386743749610857002, 3.019476368352826956 ) ) ;
#4672=ORIENTED_EDGE ( 'NONE', *, *, #379, .F. ) ;
#4674=VERTEX_POINT ( 'NONE', #1565 ) ;
#4675=ADVANCED_FACE ( 'NONE', ( #7915 ), #5903, .F. ) ;
#4676=ADVANCED_FACE ( 'NONE', ( #6653 ), #5235, .T. ) ;
#4677=FACE_OUTER_BOUND ( 'NONE', #5968, .T. ) ;
#4688=LINE ( 'NONE', #273, #1905 ) ;
#4689=ADVANCED_FACE ( 'NONE', ( #5398, #7956 ), #4627, .T. ) ;
#4694=ORIENTED_EDGE ( 'NONE', *, *, #8133, .T. ) ;
#4695=CARTESIAN_POINT ( 'NONE',  ( -1.889618362131626726E-10, 3.950000000000000178, 2.750000000234376074 ) ) ;
#4696=EDGE_LOOP ( 'NONE', ( #1190, #752, #1880, #6513 ) ) ;
#4697=DIRECTION ( 'NONE',  ( 1.000000000000000000, 0.000000000000000000, 0.000000000000000000 ) ) ;
#4698=CYLINDRICAL_SURFACE ( 'NONE', #1407, 0.2625000000000008438 ) ;
#4701=PLANE ( 'NONE',  #3851 ) ;
#4703=ADVANCED_FACE ( 'NONE', ( #7830 ), #7183, .F. ) ;
#4704=ORIENTED_EDGE ( 'NONE', *, *, #3130, .T. ) ;
#4705=CARTESIAN_POINT ( 'NONE',  ( -1.295380381263955716, 3.737605818698255700, -5.108749999999998792 ) ) ;
#4706=CARTESIAN_POINT ( 'NONE',  ( 0.3222455737775520856, 2.355994570478443517, 3.049679287146744411 ) ) ;
#4716=DIRECTION ( 'NONE',  ( 0.000000000000000000, -1.000000000000000000, -0.000000000000000000 ) ) ;
#4723=CARTESIAN_POINT ( 'NONE',  ( 1.489119987881815765, 2.223645901847905115, -2.749999999536767437 ) ) ;
#4725=PLANE ( 'NONE',  #460 ) ;
#4727=CARTESIAN_POINT ( 'NONE',  ( -1.312500000051465499, 4.908106857156239400, 2.749999995422029553 ) ) ;
#4729=CARTESIAN_POINT ( 'NONE',  ( 0.000000000000000000, 2.499999998868537521, 0.000000000000000000 ) ) ;
#4731=VERTEX_POINT ( 'NONE', #2342 ) ;
#4734=CARTESIAN_POINT ( 'NONE',  ( 0.000000000000000000, 1.664000000000000368, 2.841000000000000636 ) ) ;
#4735=ORIENTED_EDGE ( 'NONE', *, *, #7938, .T. ) ;
#4742=CARTESIAN_POINT ( 'NONE',  ( -1.310546130307260748, 3.866374246920377900, -5.108750000000002345 ) ) ;
#4743=DIRECTION ( 'NONE',  ( 0.000000000000000000, -1.000000000000000000, -0.000000000000000000 ) ) ;
#4754=DIRECTION ( 'NONE',  ( 0.000000000000000000, 0.000000000000000000, 1.000000000000000000 ) ) ;
#4761=VECTOR ( 'NONE', #3281, 39.37007874015748143 ) ;
#4764=CARTESIAN_POINT ( 'NONE',  ( 1.557862130685455426, 2.150738729487894130, -2.749999999536767437 ) ) ;
#4766=CARTESIAN_POINT ( 'NONE',  ( 0.4466248239349933646, 2.387262647126640047, -3.018973216062835085 ) ) ;
#4767=CARTESIAN_POINT ( 'NONE',  ( 1.312500000000000444, 4.908106850393701315, 0.5414159055118112907 ) ) ;
#4768=LINE ( 'NONE', #7296, #7289 ) ;
#4769=ORIENTED_EDGE ( 'NONE', *, *, #2354, .T. ) ;
#4783=VERTEX_POINT ( 'NONE', #4378 ) ;
#4789=CARTESIAN_POINT ( 'NONE',  ( -2.750000000000000444, 7.964000000000000412, 3.691250000000001030 ) ) ;
#4791=CARTESIAN_POINT ( 'NONE',  ( -0.7977802270736898960, 4.992433491425203762, -5.108750000000001457 ) ) ;
#4792=CARTESIAN_POINT ( 'NONE',  ( -0.06688424724377287078, 2.325058188798388770, 3.080150965287773879 ) ) ;
#4800=DESIGN_CONTEXT ( 'detailed design', #7847, 'design' ) ;
#4802=AXIS2_PLACEMENT_3D ( 'NONE', #1830, #6827, #3175 ) ;
#4808=ORIENTED_EDGE ( 'NONE', *, *, #5242, .T. ) ;
#4809=B_SPLINE_CURVE_WITH_KNOTS ( 'NONE', 3,
 ( #7914, #2251, #6026, #5397, #4668, #5319, #2179, #7267, #4166, #7875, #4792, #7182, #2947, #3443, #1607, #5439, #2219, #3490, #4706, #8005, #4082, #4833, #5991, #289, #7223, #368 ),
 .UNSPECIFIED., .F., .F.,
 ( 4, 2, 2, 2, 2, 2, 2, 2, 2, 2, 2, 2, 4 ),
 ( 0.000000000000000000, 0.004967431915087203512, 0.009934863830174412228, 0.01241857978771801312, 0.01490229574526161921, 0.01986972766034882792, 0.02111158563912063010, 0.02235344361789242881, 0.02483715957543602970, 0.02980459149052323842, 0.03228830744806682890, 0.03477202340561042632, 0.03973945532069762115 ),
 .UNSPECIFIED. ) ;
#4812=FACE_OUTER_BOUND ( 'NONE', #490, .T. ) ;
#4817=CARTESIAN_POINT ( 'NONE',  ( -0.7052155605301347885, 5.414000000000000590, 0.1249999999999998335 ) ) ;
#4819=ORIENTED_EDGE ( 'NONE', *, *, #1930, .F. ) ;
#4823=DIRECTION ( 'NONE',  ( 0.000000000000000000, 1.000000000000000000, 0.000000000000000000 ) ) ;
#4830=EDGE_LOOP ( 'NONE', ( #7372, #7104, #3616, #6157 ) ) ;
#4832=CARTESIAN_POINT ( 'NONE',  ( 1.500000000000000444, 5.339000000000000412, -2.750000000000000444 ) ) ;
#4833=CARTESIAN_POINT ( 'NONE',  ( 0.5066049570144357528, 2.405661888747006927, 3.000938696051032473 ) ) ;
#4843=LINE ( 'NONE', #8014, #2924 ) ;
#4845=ORIENTED_EDGE ( 'NONE', *, *, #7527, .F. ) ;
#4850=CARTESIAN_POINT ( 'NONE',  ( -0.3551829056966991915, 2.363969070009024787, -3.041846016155792753 ) ) ;
#4851=EDGE_CURVE ( 'NONE', #2209, #6986, #18, .T. ) ;
#4853=LINE ( 'NONE', #1053, #3050 ) ;
#4854=CARTESIAN_POINT ( 'NONE',  ( -1.625000000000000222, 2.217843349455980384, -2.674602989331134495 ) ) ;
#4860=CARTESIAN_POINT ( 'NONE',  ( 0.000000000000000000, 3.950000000000000178, -5.108750000000001457 ) ) ;
#4863=ORIENTED_EDGE ( 'NONE', *, *, #4976, .F. ) ;
#4876=ORIENTED_EDGE ( 'NONE', *, *, #6123, .F. ) ;
#4878=FACE_OUTER_BOUND ( 'NONE', #6534, .T. ) ;
#4885=CARTESIAN_POINT ( 'NONE',  ( 0.000000000000000000, 2.500000000000000000, 0.000000000000000000 ) ) ;
#4887=VECTOR ( 'NONE', #3500, 39.37007874015748143 ) ;
#4889=CARTESIAN_POINT ( 'NONE',  ( 3.343750000000001776, 2.500000000000000444, -0.5625000000000001110 ) ) ;
#4890=CARTESIAN_POINT ( 'NONE',  ( 1.312500000123272725, 4.908106857128372802, -5.108750000000001457 ) ) ;
#4892=CIRCLE ( 'NONE', #833, 3.343750000098590913 ) ;
#4893=CARTESIAN_POINT ( 'NONE',  ( 0.000000000000000000, 1.749999999784896065, 0.000000000000000000 ) ) ;
#4898=DIRECTION ( 'NONE',  ( 0.000000000000000000, -0.000000000000000000, 1.000000000000000000 ) ) ;
#4904=FACE_OUTER_BOUND ( 'NONE', #725, .T. ) ;
#4905=ORIENTED_EDGE ( 'NONE', *, *, #6137, .T. ) ;
#4911=CARTESIAN_POINT ( 'NONE',  ( 1.624999999811037599, 5.151388682096968097, 2.749999999536767437 ) ) ;
#4920=ORIENTED_EDGE ( 'NONE', *, *, #7883, .T. ) ;
#4927=EDGE_CURVE ( 'NONE', #1507, #445, #5148, .T. ) ;
#4928=VERTEX_POINT ( 'NONE', #1881 ) ;
#4930=ORIENTED_EDGE ( 'NONE', *, *, #730, .T. ) ;
#4931=DIRECTION ( 'NONE',  ( -0.000000000000000000, 1.000000000000000000, -0.000000000000000000 ) ) ;
#4951=ORIENTED_EDGE ( 'NONE', *, *, #2446, .T. ) ;
#4955=DIRECTION ( 'NONE',  ( -1.000000000000000000, -0.000000000000000000, -0.000000000000000000 ) ) ;
#4957=CARTESIAN_POINT ( 'NONE',  ( 2.750000000000003109, 8.588999999999998636, 2.411250000000000782 ) ) ;
#4961=DIRECTION ( 'NONE',  ( -0.000000000000000000, -1.000000000000000000, -0.000000000000000000 ) ) ;
#4966=EDGE_CURVE ( 'NONE', #6623, #4491, #4615, .T. ) ;
#4968=DIRECTION ( 'NONE',  ( -0.000000000000000000, -0.000000000000000000, 1.000000000000000000 ) ) ;
#4969=CARTESIAN_POINT ( 'NONE',  ( 1.039062322834645835, 2.913002440944882476, -4.272368937007874123 ) ) ;
#4976=EDGE_CURVE ( 'NONE', #417, #6003, #1600, .T. ) ;
#4977=EDGE_CURVE ( 'NONE', #1793, #3439, #3404, .T. ) ;
#4979=DIRECTION ( 'NONE',  ( 1.000000000000000000, 0.000000000000000000, -0.000000000000000000 ) ) ;
#4980=CARTESIAN_POINT ( 'NONE',  ( 1.625000000000000222, 2.217843350849094897, 2.674602988580442542 ) ) ;
#4986=CARTESIAN_POINT ( 'NONE',  ( 2.750000000000003109, 7.339000000000001300, 3.471636850393700513 ) ) ;
#4989=CARTESIAN_POINT ( 'NONE',  ( -1.312500000000000444, 7.352492870354978116, 3.316250000370396744 ) ) ;
#4993=CARTESIAN_POINT ( 'NONE',  ( -1.624999999999999778, 3.950000000000000178, -5.108750000000001457 ) ) ;
#4996=VERTEX_POINT ( 'NONE', #5308 ) ;
#4997=FACE_OUTER_BOUND ( 'NONE', #6788, .T. ) ;
#4998=ADVANCED_FACE ( 'NONE', ( #7089 ), #4002, .F. ) ;
#4999=DIRECTION ( 'NONE',  ( -1.000000000000000000, 0.000000000000000000, -0.000000000000000000 ) ) ;
#5000=CIRCLE ( 'NONE', #14, 1.624999999999999778 ) ;
#5005=DIRECTION ( 'NONE',  ( -1.000000000000000000, 0.000000000000000000, -0.000000000000000000 ) ) ;
#5006=CARTESIAN_POINT ( 'NONE',  ( 1.177243228188373791, 3.368106800967091807, -5.108749999999999680 ) ) ;
#5013=CIRCLE ( 'NONE', #4223, 1.624999999999999778 ) ;
#5016=CARTESIAN_POINT ( 'NONE',  ( -2.946793808642157231, 2.500000000130568889, -0.5624999991015005030 ) ) ;
#5028=DIRECTION ( 'NONE',  ( 1.000000000000000000, -1.681137231067760553E-15, 0.000000000000000000 ) ) ;
#5030=DIRECTION ( 'NONE',  ( 0.000000000000000000, -1.000000000000000000, 0.000000000000000000 ) ) ;
#5041=CARTESIAN_POINT ( 'NONE',  ( -1.312500000000000444, 7.352492870354978116, 3.316250000000001474 ) ) ;
#5042=LINE ( 'NONE', #7019, #4237 ) ;
#5047=AXIS2_PLACEMENT_3D ( 'NONE', #4695, #983, #5976 ) ;
#5049=CARTESIAN_POINT ( 'NONE',  ( 0.6955817875586080001, 5.063844427419111227, -5.108750000000004121 ) ) ;
#5055=AXIS2_PLACEMENT_3D ( 'NONE', #4435, #1860, #7514 ) ;
#5056=VECTOR ( 'NONE', #2613, 39.37007874015748143 ) ;
#5059=CARTESIAN_POINT ( 'NONE',  ( 0.000000000000000000, 1.749999999784895843, 0.000000000000000000 ) ) ;
#5060=CARTESIAN_POINT ( 'NONE',  ( -2.749999999999998668, 7.338999999999999524, 3.471636850393700513 ) ) ;
#5067=CARTESIAN_POINT ( 'NONE',  ( 3.179822820549663476, 2.000074506952454811, 0.5624999982029994516 ) ) ;
#5070=DIRECTION ( 'NONE',  ( 0.000000000000000000, 0.000000000000000000, 1.000000000000000000 ) ) ;
#5077=B_SPLINE_CURVE_WITH_KNOTS ( 'NONE', 3,
 ( #2268, #268, #1586, #7804, #3465, #5965, #4766, #7294, #1663, #4515, #3249, #123 ),
 .UNSPECIFIED., .F., .F.,
 ( 4, 2, 2, 2, 2, 4 ),
 ( 8.673617379884035472E-18, 0.004953213565686583227, 0.009906427131373157779, 0.01238303391421645416, 0.01485964069705974881, 0.01981285426274633638 ),
 .UNSPECIFIED. ) ;
#5091=CARTESIAN_POINT ( 'NONE',  ( 1.304290195953534237, 4.098156632275986588, -5.108750000000004121 ) ) ;
#5094=ORIENTED_EDGE ( 'NONE', *, *, #7384, .T. ) ;
#5095=EDGE_CURVE ( 'NONE', #2223, #2302, #6098, .T. ) ;
#5096=DIRECTION ( 'NONE',  ( 0.000000000000000000, 1.000000000000000000, 0.000000000000000000 ) ) ;
#5101=PLANE ( 'NONE',  #7838 ) ;
#5109=CARTESIAN_POINT ( 'NONE',  ( -3.343750000000002220, 2.500000000000000444, 0.5625000000000003331 ) ) ;
#5118=ORIENTED_EDGE ( 'NONE', *, *, #216, .F. ) ;
#5127=CARTESIAN_POINT ( 'NONE',  ( 1.102289196576730079, 3.237202587873624360, -5.108750000000004121 ) ) ;
#5129=FACE_OUTER_BOUND ( 'NONE', #5388, .T. ) ;
#5132=CARTESIAN_POINT ( 'NONE',  ( 1.312500000000000444, 5.969165905511811587, 3.161250000000001670 ) ) ;
#5134=ORIENTED_EDGE ( 'NONE', *, *, #3657, .F. ) ;
#5137=CARTESIAN_POINT ( 'NONE',  ( 0.000000000000000000, 3.950000000000000178, 3.691250000234376660 ) ) ;
#5142=ORIENTED_EDGE ( 'NONE', *, *, #3732, .T. ) ;
#5144=CARTESIAN_POINT ( 'NONE',  ( -2.946793808531571468, 2.500000000000000000, 0.5625000000000002220 ) ) ;
#5145=LINE ( 'NONE', #2618, #6640 ) ;
#5148=LINE ( 'NONE', #7696, #1107 ) ;
#5149=ORIENTED_EDGE ( 'NONE', *, *, #7167, .F. ) ;
#5151=CARTESIAN_POINT ( 'NONE',  ( 0.000000000000000000, 5.113999999999999879, 0.000000000000000000 ) ) ;
#5159=CARTESIAN_POINT ( 'NONE',  ( 1.500000000000000444, 5.113999999999999879, -2.750000000000000444 ) ) ;
#5161=EDGE_LOOP ( 'NONE', ( #2781, #2389 ) ) ;
#5164=CIRCLE ( 'NONE', #4111, 3.000000000065115024 ) ;
#5170=FACE_OUTER_BOUND ( 'NONE', #8028, .T. ) ;
#5174=EDGE_LOOP ( 'NONE', ( #3697, #7644, #3091, #6446 ) ) ;
#5179=AXIS2_PLACEMENT_3D ( 'NONE', #2809, #2318, #5916 ) ;
#5182=DIRECTION ( 'NONE',  ( 0.000000000000000000, 0.000000000000000000, -1.000000000000000000 ) ) ;
#5188=CARTESIAN_POINT ( 'NONE',  ( 0.000000000000000000, 3.950000000000000178, 2.750000000234376074 ) ) ;
#5196=VERTEX_POINT ( 'NONE', #3864 ) ;
#5197=DIRECTION ( 'NONE',  ( 0.000000000000000000, -0.000000000000000000, -1.000000000000000000 ) ) ;
#5199=CARTESIAN_POINT ( 'NONE',  ( -1.625000000000000222, 5.639000000000001123, 0.1249999999999997641 ) ) ;
#5206=DIRECTION ( 'NONE',  ( 0.000000000000000000, 0.000000000000000000, -1.000000000000000000 ) ) ;
#5211=ORIENTED_EDGE ( 'NONE', *, *, #5849, .T. ) ;
#5213=DIRECTION ( 'NONE',  ( 0.000000000000000000, -1.000000000000000000, 0.000000000000000000 ) ) ;
#5214=CARTESIAN_POINT ( 'NONE',  ( -2.749999999999999556, 8.589000000000000412, 3.243476614173228967 ) ) ;
#5217=DIRECTION ( 'NONE',  ( -0.000000000000000000, 0.000000000000000000, -1.000000000000000000 ) ) ;
#5219=PLANE ( 'NONE',  #7942 ) ;
#5221=ADVANCED_FACE ( 'NONE', ( #1987 ), #6994, .F. ) ;
#5223=CARTESIAN_POINT ( 'NONE',  ( 0.000000000000000000, 3.950000000000000178, -4.308749999765625560 ) ) ;
#5226=VERTEX_POINT ( 'NONE', #4406 ) ;
#5227=CARTESIAN_POINT ( 'NONE',  ( 1.624999999999999556, 2.076218724953421191, -2.749999999536766992 ) ) ;
#5229=DIRECTION ( 'NONE',  ( 0.000000000000000000, 0.000000000000000000, -1.000000000000000000 ) ) ;
#5230=LINE ( 'NONE', #6356, #6888 ) ;
#5233=CARTESIAN_POINT ( 'NONE',  ( -1.624999999371729231, 2.076218724780642511, 2.750000000000000444 ) ) ;
#5234=DIRECTION ( 'NONE',  ( 0.000000000000000000, 0.000000000000000000, 1.000000000000000000 ) ) ;
#5235=PLANE ( 'NONE',  #34 ) ;
#5236=CARTESIAN_POINT ( 'NONE',  ( -2.750000000000000444, 7.339000000000001300, 3.161250000000001670 ) ) ;
#5238=ORIENTED_EDGE ( 'NONE', *, *, #279, .F. ) ;
#5242=EDGE_CURVE ( 'NONE', #5914, #6240, #6948, .T. ) ;
#5250=ORIENTED_EDGE ( 'NONE', *, *, #6953, .T. ) ;
#5252=CARTESIAN_POINT ( 'NONE',  ( 2.537500000000000533, 2.500000000000000444, -0.2625000000000008438 ) ) ;
#5255=CARTESIAN_POINT ( 'NONE',  ( -1.557862129405290341, 2.150738729984251307, -2.750000000000000444 ) ) ;
#5257=ORIENTED_EDGE ( 'NONE', *, *, #162, .T. ) ;
#5259=VECTOR ( 'NONE', #8013, 39.37007874015748143 ) ;
#5261=EDGE_CURVE ( 'NONE', #4377, #1364, #7679, .T. ) ;
#5264=CARTESIAN_POINT ( 'NONE',  ( 1.625000000000000222, 2.217843349262734076, -2.674602989435063805 ) ) ;
#5265=VERTEX_POINT ( 'NONE', #5016 ) ;
#5269=VECTOR ( 'NONE', #3575, 39.37007874015748143 ) ;
#5273=CARTESIAN_POINT ( 'NONE',  ( -0.6588841106301542849, 2.814050781761043840, -5.108750000000002345 ) ) ;
#5276=DIRECTION ( 'NONE',  ( -0.000000000000000000, 1.000000000000000000, 0.000000000000000000 ) ) ;
#5278=CARTESIAN_POINT ( 'NONE',  ( -1.312500000000000222, 8.589000000000002188, 3.161250000126027970 ) ) ;
#5281=ORIENTED_EDGE ( 'NONE', *, *, #5387, .T. ) ;
#5285=DIRECTION ( 'NONE',  ( -1.000000000000000000, 0.000000000000000000, 0.000000000000000000 ) ) ;
#5286=EDGE_CURVE ( 'NONE', #6986, #7136, #7580, .T. ) ;
#5288=VECTOR ( 'NONE', #7217, 39.37007874015748143 ) ;
#5289=CLOSED_SHELL ( 'NONE', ( #2875, #2231, #398, #4221, #993, #3548, #2286, #6668, #1084, #4121, #4382, #4321, #8115, #190, #7435, #2638, #3978, #4676, #6789, #2082, #1433, #2026, #4689, #6575, #366, #4675, #8062, #1232, #3171, #781, #42, #899, #1221, #7797, #5638, #1572, #6153, #3507, #2057, #2687, #4220, #5324, #5948, #5221, #118, #4998, #5434, #1285, #7002, #487, #1740, #3012, #4703, #1585, #2280, #8, #1040, #6440, #6404, #13, #7141, #3294, #6276, #36, #3682, #7767 ) ) ;
#5291=ORIENTED_EDGE ( 'NONE', *, *, #1660, .F. ) ;
#5292=VECTOR ( 'NONE', #5217, 39.37007874015748143 ) ;
#5295=DIRECTION ( 'NONE',  ( 1.000000000000000000, 0.000000000000000000, 0.000000000000000000 ) ) ;
#5302=EDGE_LOOP ( 'NONE', ( #4576, #2373, #6374, #6246, #6525, #5447, #1558, #1604, #7330, #1484, #3811, #1448 ) ) ;
#5305=VECTOR ( 'NONE', #746, 39.37007874015748143 ) ;
#5307=ORIENTED_EDGE ( 'NONE', *, *, #6299, .F. ) ;
#5308=CARTESIAN_POINT ( 'NONE',  ( 1.500000000000000444, 5.113999999999999879, 2.750000000058594907 ) ) ;
#5312=DIRECTION ( 'NONE',  ( 0.000000000000000000, -0.000000000000000000, 1.000000000000000000 ) ) ;
#5314=ORIENTED_EDGE ( 'NONE', *, *, #3888, .F. ) ;
#5318=CARTESIAN_POINT ( 'NONE',  ( -0.8008852849046133038, 2.909290603415537024, -5.108749999999998792 ) ) ;
#5319=CARTESIAN_POINT ( 'NONE',  ( -0.3549540556708988270, 2.363917302189245451, 3.041896893698089244 ) ) ;
#5324=ADVANCED_FACE ( 'NONE', ( #3935 ), #2693, .F. ) ;
#5333=EDGE_CURVE ( 'NONE', #3004, #8024, #992, .T. ) ;
#5335=CARTESIAN_POINT ( 'NONE',  ( 1.347488133582466441, 2.365290550890831067, -2.749999999536767437 ) ) ;
#5341=CARTESIAN_POINT ( 'NONE',  ( 2.750000000000000444, 8.574153543316302972, 3.323749999966777668 ) ) ;
#5343=ORIENTED_EDGE ( 'NONE', *, *, #6835, .F. ) ;
#5345=LINE ( 'NONE', #6527, #5833 ) ;
#5350=CARTESIAN_POINT ( 'NONE',  ( 0.000000000000000000, 3.950000000000000178, 3.691250000234376660 ) ) ;
#5356=CARTESIAN_POINT ( 'NONE',  ( 1.625000000000000222, 3.950000000000000178, -2.750000000000000444 ) ) ;
#5358=LINE ( 'NONE', #7783, #448 ) ;
#5368=CARTESIAN_POINT ( 'NONE',  ( -2.750000000000000444, 7.964000000000000412, 3.691250000000001030 ) ) ;
#5381=DIRECTION ( 'NONE',  ( 1.000000000000000000, 0.000000000000000000, -0.000000000000000000 ) ) ;
#5387=EDGE_CURVE ( 'NONE', #1923, #2064, #5966, .T. ) ;
#5388=EDGE_LOOP ( 'NONE', ( #2434, #762, #8157, #6630 ) ) ;
#5391=ORIENTED_EDGE ( 'NONE', *, *, #4387, .F. ) ;
#5393=DIRECTION ( 'NONE',  ( -0.000000000000000000, -0.000000000000000000, 1.000000000000000000 ) ) ;
#5394=CIRCLE ( 'NONE', #1866, 2.841000000000000636 ) ;
#5397=CARTESIAN_POINT ( 'NONE',  ( -0.5081896104144416615, 2.405274364305883150, 3.001302249876916406 ) ) ;
#5398=FACE_BOUND ( 'NONE', #1060, .T. ) ;
#5401=ORIENTED_EDGE ( 'NONE', *, *, #3820, .F. ) ;
#5416=AXIS2_PLACEMENT_3D ( 'NONE', #5151, #3154, #2051 ) ;
#5426=EDGE_LOOP ( 'NONE', ( #5401, #429, #640, #900 ) ) ;
#5428=CARTESIAN_POINT ( 'NONE',  ( -1.624999999999999778, 3.950000000000000178, -5.108750000000001457 ) ) ;
#5431=ORIENTED_EDGE ( 'NONE', *, *, #78, .F. ) ;
#5434=ADVANCED_FACE ( 'NONE', ( #7894 ), #4725, .F. ) ;
#5437=ORIENTED_EDGE ( 'NONE', *, *, #4497, .T. ) ;
#5439=CARTESIAN_POINT ( 'NONE',  ( 0.1300012438279209703, 2.329874691800032149, 3.075403168634932349 ) ) ;
#5441=ADVANCED_BREP_SHAPE_REPRESENTATION ( '', ( #7251, #7272 ), #2811 ) ;
#5444=CIRCLE ( 'NONE', #3998, 3.343750000000001332 ) ;
#5447=ORIENTED_EDGE ( 'NONE', *, *, #2634, .T. ) ;
#5452=DIRECTION ( 'NONE',  ( 0.000000000000000000, 0.000000000000000000, -1.000000000000000000 ) ) ;
#5455=CARTESIAN_POINT ( 'NONE',  ( -3.296097360979716839, 1.749999999818133034, 0.5625000000000002220 ) ) ;
#5463=CARTESIAN_POINT ( 'NONE',  ( -1.624999999336056877, 2.076218724820237060, -2.750000000000000444 ) ) ;
#5464=ORIENTED_EDGE ( 'NONE', *, *, #1193, .F. ) ;
#5467=ORIENTED_EDGE ( 'NONE', *, *, #7681, .T. ) ;
#5469=CARTESIAN_POINT ( 'NONE',  ( -3.343750000000001776, 0.000000000000000000, -0.5624999982030005619 ) ) ;
#5471=ORIENTED_EDGE ( 'NONE', *, *, #4641, .F. ) ;
#5475=CARTESIAN_POINT ( 'NONE',  ( -0.1707770274186259651, 5.254148146219773885, -5.108750000000001457 ) ) ;
#5482=CARTESIAN_POINT ( 'NONE',  ( 2.187663376927555706E-18, 3.950000000000000178, 0.1249999999999997641 ) ) ;
#5483=EDGE_LOOP ( 'NONE', ( #3843, #7609 ) ) ;
#5485=DIRECTION ( 'NONE',  ( 1.000000000000000000, 0.000000000000000000, -0.000000000000000000 ) ) ;
#5493=EDGE_CURVE ( 'NONE', #7297, #3620, #4892, .T. ) ;
#5495=DIRECTION ( 'NONE',  ( -0.000000000000000000, 1.000000000000000000, 0.000000000000000000 ) ) ;
#5496=EDGE_LOOP ( 'NONE', ( #1402, #5134, #1281, #2133 ) ) ;
#5499=LINE ( 'NONE', #1202, #3061 ) ;
#5501=LINE ( 'NONE', #7511, #3737 ) ;
#5504=PLANE ( 'NONE',  #6235 ) ;
#5505=EDGE_CURVE ( 'NONE', #5594, #2439, #1367, .T. ) ;
#5512=CARTESIAN_POINT ( 'NONE',  ( 0.7335700393700786970, 2.500000000000000444, 2.909883779527559611 ) ) ;
#5516=EDGE_CURVE ( 'NONE', #6151, #3620, #4853, .T. ) ;
#5528=ORIENTED_EDGE ( 'NONE', *, *, #3289, .T. ) ;
#5536=VECTOR ( 'NONE', #3834, 39.37007874015748143 ) ;
#5543=EDGE_LOOP ( 'NONE', ( #170, #6432, #2561, #4819, #6022, #1013 ) ) ;
#5549=EDGE_CURVE ( 'NONE', #2981, #6439, #7931, .T. ) ;
#5550=EDGE_LOOP ( 'NONE', ( #2085, #5343, #904, #4059, #4876, #3128, #2636, #2694, #5118, #90, #4643, #5211 ) ) ;
#5554=FACE_OUTER_BOUND ( 'NONE', #6665, .T. ) ;
#5564=CARTESIAN_POINT ( 'NONE',  ( 0.000000000000000000, 2.325000000000000622, -3.080208333333334103 ) ) ;
#5565=DIRECTION ( 'NONE',  ( 0.000000000000000000, 0.000000000000000000, -1.000000000000000000 ) ) ;
#5570=CARTESIAN_POINT ( 'NONE',  ( 2.750000000000000444, 7.531471846334603981, 3.702890677416158294 ) ) ;
#5571=DIRECTION ( 'NONE',  ( -0.000000000000000000, -0.000000000000000000, 1.000000000000000000 ) ) ;
#5576=EDGE_CURVE ( 'NONE', #266, #7256, #6782, .T. ) ;
#5578=CARTESIAN_POINT ( 'NONE',  ( 1.500000000000000444, 5.339000000000000412, -2.750000000000000444 ) ) ;
#5583=ORIENTED_EDGE ( 'NONE', *, *, #5584, .F. ) ;
#5584=EDGE_CURVE ( 'NONE', #6974, #6859, #4626, .T. ) ;
#5586=EDGE_CURVE ( 'NONE', #6055, #6810, #1741, .T. ) ;
#5587=CARTESIAN_POINT ( 'NONE',  ( -0.6797036848942895615, 2.472748453411862446, -2.935395484029501123 ) ) ;
#5588=DIRECTION ( 'NONE',  ( 0.000000000000000000, -1.000000000000000000, 0.000000000000000000 ) ) ;
#5591=CIRCLE ( 'NONE', #7462, 2.841000000000000636 ) ;
#5593=CARTESIAN_POINT ( 'NONE',  ( -1.312500000000000444, 5.969165905511811587, 3.161250000000001670 ) ) ;
#5594=VERTEX_POINT ( 'NONE', #2450 ) ;
#5597=CARTESIAN_POINT ( 'NONE',  ( 2.750000000000000444, 8.574153543316302972, 3.323749999966777668 ) ) ;
#5606=CARTESIAN_POINT ( 'NONE',  ( -3.296097360979716839, 1.749999999818133034, 0.5625000000000002220 ) ) ;
#5614=DIRECTION ( 'NONE',  ( 1.000000000000000000, 0.000000000000000000, 0.000000000000000000 ) ) ;
#5617=CARTESIAN_POINT ( 'NONE',  ( -3.179822820373745085, 2.000074507330735329, -0.5624999982030005619 ) ) ;
#5618=DIRECTION ( 'NONE',  ( 1.000000000000000000, 0.000000000000000000, 0.000000000000000000 ) ) ;
#5622=LINE ( 'NONE', #2998, #6728 ) ;
#5624=CARTESIAN_POINT ( 'NONE',  ( 0.9878476365635346923, 3.081585747833998745, -5.108750000000003233 ) ) ;
#5631=CARTESIAN_POINT ( 'NONE',  ( 1.624999999999999778, 3.950000000000000178, -5.108750000000001457 ) ) ;
#5637=CARTESIAN_POINT ( 'NONE',  ( -1.274606804509407887, 2.434036455836466217, 2.750000000000000444 ) ) ;
#5638=ADVANCED_FACE ( 'NONE', ( #209 ), #2750, .F. ) ;
#5640=DIRECTION ( 'NONE',  ( -0.000000000000000000, 1.000000000000000000, -0.000000000000000000 ) ) ;
#5642=EDGE_LOOP ( 'NONE', ( #6717, #6138, #5830, #5978, #2047, #1734 ) ) ;
#5650=DIRECTION ( 'NONE',  ( 0.000000000000000000, 0.000000000000000000, 1.000000000000000000 ) ) ;
#5652=VECTOR ( 'NONE', #7889, 39.37007874015748143 ) ;
#5658=CARTESIAN_POINT ( 'NONE',  ( -0.6239339750438661625, 2.448288917813445487, -2.959250064740976960 ) ) ;
#5660=CARTESIAN_POINT ( 'NONE',  ( 1.301660623806975448, 4.119709289672806030, -5.108750000000004121 ) ) ;
#5662=ORIENTED_EDGE ( 'NONE', *, *, #4625, .F. ) ;
#5664=ORIENTED_EDGE ( 'NONE', *, *, #4040, .F. ) ;
#5665=CARTESIAN_POINT ( 'NONE',  ( -2.750000000000000444, 8.574153543306394454, 3.323750000003751648 ) ) ;
#5666=CARTESIAN_POINT ( 'NONE',  ( 0.000000000000000000, 2.500000000000000000, 0.000000000000000000 ) ) ;
#5668=ORIENTED_EDGE ( 'NONE', *, *, #4634, .F. ) ;
#5680=CARTESIAN_POINT ( 'NONE',  ( 3.296097361251832503, 1.749999999892448477, 0.5624999982029994516 ) ) ;
#5683=EDGE_CURVE ( 'NONE', #47, #6151, #786, .T. ) ;
#5687=DIRECTION ( 'NONE',  ( 0.000000000000000000, 0.000000000000000000, 1.000000000000000000 ) ) ;
#5695=ORIENTED_EDGE ( 'NONE', *, *, #8098, .F. ) ;
#5704=CIRCLE ( 'NONE', #2704, 1.249999999999999556 ) ;
#5709=DIRECTION ( 'NONE',  ( 0.000000000000000000, 0.000000000000000000, -1.000000000000000000 ) ) ;
#5710=CARTESIAN_POINT ( 'NONE',  ( 0.7455319525492740684, 2.869584312975302254, -5.108750000000003233 ) ) ;
#5714=VECTOR ( 'NONE', #3101, 39.37007874015748143 ) ;
#5716=ORIENTED_EDGE ( 'NONE', *, *, #3820, .T. ) ;
#5719=CYLINDRICAL_SURFACE ( 'NONE', #7456, 1.624999999999999778 ) ;
#5723=ORIENTED_EDGE ( 'NONE', *, *, #1977, .T. ) ;
#5727=CARTESIAN_POINT ( 'NONE',  ( 2.750000000000000000, 7.521783347043601964, 3.691250000474207038 ) ) ;
#5728=CARTESIAN_POINT ( 'NONE',  ( -0.8969581913071023038, 4.909142736075838620, -5.108749999999997904 ) ) ;
#5730=ORIENTED_EDGE ( 'NONE', *, *, #3289, .F. ) ;
#5731=CARTESIAN_POINT ( 'NONE',  ( -2.750000000000000444, 7.964000000000000412, 3.691250000000001030 ) ) ;
#5733=VERTEX_POINT ( 'NONE', #3324 ) ;
#5735=EDGE_CURVE ( 'NONE', #5265, #2302, #7747, .T. ) ;
#5738=CARTESIAN_POINT ( 'NONE',  ( -0.7455319445466856987, 5.030415712794154892, -5.108750000000001457 ) ) ;
#5748=VERTEX_POINT ( 'NONE', #1483 ) ;
#5752=EDGE_CURVE ( 'NONE', #7868, #540, #4593, .T. ) ;
#5753=CARTESIAN_POINT ( 'NONE',  ( 0.2166614821407901181, 5.245203122673235185, -5.108749999999999680 ) ) ;
#5756=ORIENTED_EDGE ( 'NONE', *, *, #5549, .T. ) ;
#5759=CARTESIAN_POINT ( 'NONE',  ( 3.343750000000002220, 2.499999999622846136, 0.5624999994009998172 ) ) ;
#5767=EDGE_CURVE ( 'NONE', #4304, #5914, #585, .T. ) ;
#5775=FACE_OUTER_BOUND ( 'NONE', #2874, .T. ) ;
#5777=ORIENTED_EDGE ( 'NONE', *, *, #4375, .T. ) ;
#5779=LINE ( 'NONE', #2008, #4761 ) ;
#5789=CARTESIAN_POINT ( 'NONE',  ( 0.4244988595014765331, 5.194936639113962862, -5.108750000000002345 ) ) ;
#5796=CARTESIAN_POINT ( 'NONE',  ( 0.000000000000000000, 3.950000000000000178, 2.750000000000000888 ) ) ;
#5797=VECTOR ( 'NONE', #6181, 39.37007874015748143 ) ;
#5800=VECTOR ( 'NONE', #7449, 39.37007874015748143 ) ;
#5806=DIRECTION ( 'NONE',  ( 1.000000000000000000, 0.000000000000000000, -0.000000000000000000 ) ) ;
#5809=AXIS2_PLACEMENT_3D ( 'NONE', #7891, #6083, #4102 ) ;
#5820=AXIS2_PLACEMENT_3D ( 'NONE', #1972, #1357, #3847 ) ;
#5823=CARTESIAN_POINT ( 'NONE',  ( -1.304290195246832873, 3.801843365448688505, -5.108750000000001457 ) ) ;
#5824=DIRECTION ( 'NONE',  ( 0.000000000000000000, -1.000000000000000000, 0.000000000000000000 ) ) ;
#5825=CARTESIAN_POINT ( 'NONE',  ( 2.750000000000000888, 8.589000000000000412, 3.243476614173229411 ) ) ;
#5830=ORIENTED_EDGE ( 'NONE', *, *, #1035, .T. ) ;
#5831=CARTESIAN_POINT ( 'NONE',  ( 0.000000000000000000, 5.414000000000000590, 0.000000000000000000 ) ) ;
#5833=VECTOR ( 'NONE', #897, 39.37007874015748143 ) ;
#5846=CARTESIAN_POINT ( 'NONE',  ( -2.749999999999999556, 8.589000000000000412, 3.161250000000001670 ) ) ;
#5847=CIRCLE ( 'NONE', #873, 1.624999995942718156 ) ;
#5848=ORIENTED_EDGE ( 'NONE', *, *, #2686, .T. ) ;
#5849=EDGE_CURVE ( 'NONE', #4298, #4397, #5904, .T. ) ;
#5857=AXIS2_PLACEMENT_3D ( 'NONE', #1951, #4442, #3823 ) ;
#5858=VERTEX_POINT ( 'NONE', #4047 ) ;
#5861=ORIENTED_EDGE ( 'NONE', *, *, #5333, .T. ) ;
#5864=LINE ( 'NONE', #2743, #6124 ) ;
#5867=ORIENTED_EDGE ( 'NONE', *, *, #7157, .F. ) ;
#5869=DIRECTION ( 'NONE',  ( -0.000000000000000000, 1.000000000000000000, -0.000000000000000000 ) ) ;
#5870=SHAPE_REPRESENTATION_RELATIONSHIP ( 'NONE' , 'NONE' ,  #6505, #5441 ) ;
#5874=ORIENTED_EDGE ( 'NONE', *, *, #6299, .T. ) ;
#5875=DIRECTION ( 'NONE',  ( 0.000000000000000000, -0.9090648228942841413, -0.4166547104932138423 ) ) ;
#5877=LINE ( 'NONE', #6001, #7941 ) ;
#5886=EDGE_CURVE ( 'NONE', #7545, #6458, #6232, .T. ) ;
#5887=CARTESIAN_POINT ( 'NONE',  ( 2.750000000000000444, 7.964000000000001300, 3.691250000000001030 ) ) ;
#5897=FACE_OUTER_BOUND ( 'NONE', #222, .T. ) ;
#5899=VERTEX_POINT ( 'NONE', #3564 ) ;
#5902=CARTESIAN_POINT ( 'NONE',  ( -0.8990231271313871009, 2.992770062582230661, -5.108749999999997904 ) ) ;
#5903=PLANE ( 'NONE',  #4628 ) ;
#5904=LINE ( 'NONE', #292, #179 ) ;
#5914=VERTEX_POINT ( 'NONE', #2832 ) ;
#5916=DIRECTION ( 'NONE',  ( 1.000000000000000000, 0.000000000000000000, 0.000000000000000000 ) ) ;
#5917=CARTESIAN_POINT ( 'NONE',  ( 0.000000000000000000, 3.950000000000000178, 3.691250000234376216 ) ) ;
#5918=DIRECTION ( 'NONE',  ( -0.000000000000000000, -0.000000000000000000, 1.000000000000000000 ) ) ;
#5923=DIRECTION ( 'NONE',  ( -0.000000000000000000, 0.000000000000000000, -1.000000000000000000 ) ) ;
#5927=ORIENTED_EDGE ( 'NONE', *, *, #6989, .F. ) ;
#5930=VECTOR ( 'NONE', #6742, 39.37007874015748143 ) ;
#5932=DIRECTION ( 'NONE',  ( 1.000000000000000000, -0.000000000000000000, 0.000000000000000000 ) ) ;
#5934=CARTESIAN_POINT ( 'NONE',  ( 1.625000000000000222, 2.500000000000000000, -2.521780125229002412 ) ) ;
#5940=AXIS2_PLACEMENT_3D ( 'NONE', #103, #1959, #5070 ) ;
#5942=EDGE_CURVE ( 'NONE', #3004, #1632, #7495, .T. ) ;
#5943=CARTESIAN_POINT ( 'NONE',  ( -0.9907400750648208687, 3.084787739353607172, -5.108749999999999680 ) ) ;
#5944=DIRECTION ( 'NONE',  ( 0.000000000000000000, -0.000000000000000000, 1.000000000000000000 ) ) ;
#5948=ADVANCED_FACE ( 'NONE', ( #2384 ), #6768, .F. ) ;
#5960=ORIENTED_EDGE ( 'NONE', *, *, #1584, .T. ) ;
#5961=CIRCLE ( 'NONE', #7704, 2.841000000000000636 ) ;
#5963=FACE_BOUND ( 'NONE', #7178, .T. ) ;
#5964=LINE ( 'NONE', #1621, #1270 ) ;
#5965=CARTESIAN_POINT ( 'NONE',  ( 0.4157371843214867635, 2.378754802131286095, -3.027323041911860635 ) ) ;
#5966=LINE ( 'NONE', #2111, #6626 ) ;
#5968=EDGE_LOOP ( 'NONE', ( #2565, #6564 ) ) ;
#5971=VECTOR ( 'NONE', #8026, 39.37007874015748143 ) ;
#5976=DIRECTION ( 'NONE',  ( -1.000000000000000000, 0.000000000000000000, -0.000000000000000000 ) ) ;
#5978=ORIENTED_EDGE ( 'NONE', *, *, #1955, .F. ) ;
#5989=AXIS2_PLACEMENT_3D ( 'NONE', #6256, #6868, #1259 ) ;
#5990=CARTESIAN_POINT ( 'NONE',  ( -0.5830436547479556086, 2.773322901827991682, -5.108750000000002345 ) ) ;
#5991=CARTESIAN_POINT ( 'NONE',  ( 0.5362929982961579523, 2.415731535078691206, 2.991079242820094297 ) ) ;
#5992=LINE ( 'NONE', #3361, #4371 ) ;
#5995=CARTESIAN_POINT ( 'NONE',  ( -1.312500000000000888, 7.964000000000000412, 2.411250000000000338 ) ) ;
#5997=ORIENTED_EDGE ( 'NONE', *, *, #3251, .F. ) ;
#6001=CARTESIAN_POINT ( 'NONE',  ( 0.000000000000000000, 8.574153543307087233, 3.323750000000000870 ) ) ;
#6003=VERTEX_POINT ( 'NONE', #2344 ) ;
#6011=FACE_OUTER_BOUND ( 'NONE', #5550, .T. ) ;
#6014=PLANE ( 'NONE',  #1644 ) ;
#6018=( BOUNDED_CURVE ( )  B_SPLINE_CURVE ( 2, ( #2771, #1018, #1057, #3514, #3593, #4151, #6092 ),
 .UNSPECIFIED., .F., .F. ) 
 B_SPLINE_CURVE_WITH_KNOTS ( ( 3, 2, 2, 3 ),
 ( 1.018141215013587730E-11, 0.003869794778861493714, 0.03119827453828998703, 0.05852675429817026653 ),
 .UNSPECIFIED. ) 
 CURVE ( )  GEOMETRIC_REPRESENTATION_ITEM ( )  RATIONAL_B_SPLINE_CURVE ( ( 0.9287967261194141066, 0.9585254410079242504, 1.000000000000000000, 0.7071067811865479058, 1.000000000000000000, 0.7071067811865479058, 1.000000000000000000 ) ) 
 REPRESENTATION_ITEM ( '' )  );
#6022=ORIENTED_EDGE ( 'NONE', *, *, #1642, .F. ) ;
#6023=LINE ( 'NONE', #408, #480 ) ;
#6026=CARTESIAN_POINT ( 'NONE',  ( -0.6238927636269362420, 2.448270400771923594, 2.959268117001225384 ) ) ;
#6028=DIRECTION ( 'NONE',  ( 0.000000000000000000, 1.000000000000000000, -0.000000000000000000 ) ) ;
#6029=CARTESIAN_POINT ( 'NONE',  ( -2.750000000000000444, 7.338999999999999524, 3.471636850393701401 ) ) ;
#6031=CARTESIAN_POINT ( 'NONE',  ( -1.312500000000000444, 7.339000000000003077, 2.411250000000000782 ) ) ;
#6041=DIRECTION ( 'NONE',  ( -0.000000000000000000, 1.000000000000000000, -0.000000000000000000 ) ) ;
#6050=LINE ( 'NONE', #6133, #7437 ) ;
#6052=ORIENTED_EDGE ( 'NONE', *, *, #5576, .T. ) ;
#6055=VERTEX_POINT ( 'NONE', #6110 ) ;
#6060=EDGE_LOOP ( 'NONE', ( #2922, #5471, #2311 ) ) ;
#6061=VECTOR ( 'NONE', #1735, 39.37007874015748143 ) ;
#6064=DIRECTION ( 'NONE',  ( 0.000000000000000000, 0.000000000000000000, -1.000000000000000000 ) ) ;
#6070=VECTOR ( 'NONE', #667, 39.37007874015748143 ) ;
#6079=ORIENTED_EDGE ( 'NONE', *, *, #337, .T. ) ;
#6083=DIRECTION ( 'NONE',  ( 0.000000000000000000, 0.000000000000000000, -1.000000000000000000 ) ) ;
#6086=AXIS2_PLACEMENT_3D ( 'NONE', #1383, #761, #4979 ) ;
#6091=CARTESIAN_POINT ( 'NONE',  ( 0.000000000000000000, 2.500000000000000000, 2.749999999536767437 ) ) ;
#6092=CARTESIAN_POINT ( 'NONE',  ( 1.312500000000000444, 8.589000000000002188, 3.161250000147724837 ) ) ;
#6098=LINE ( 'NONE', #5469, #7967 ) ;
#6103=LINE ( 'NONE', #608, #7965 ) ;
#6106=CARTESIAN_POINT ( 'NONE',  ( 0.000000000000000000, 5.414000000000000590, 0.1249999999999999029 ) ) ;
#6110=CARTESIAN_POINT ( 'NONE',  ( 2.750000000000000444, 7.964000000000001300, 3.323749999955704304 ) ) ;
#6118=CARTESIAN_POINT ( 'NONE',  ( -1.625000000000000222, 3.950000000000000178, -2.750000000000000444 ) ) ;
#6120=ORIENTED_EDGE ( 'NONE', *, *, #6137, .F. ) ;
#6121=FACE_OUTER_BOUND ( 'NONE', #6465, .T. ) ;
#6122=EDGE_LOOP ( 'NONE', ( #6197, #5723, #3970, #2895 ) ) ;
#6123=EDGE_CURVE ( 'NONE', #1507, #5196, #618, .T. ) ;
#6124=VECTOR ( 'NONE', #1350, 39.37007874015748143 ) ;
#6125=CARTESIAN_POINT ( 'NONE',  ( 2.946793808523474834, 2.500000000017352786, -0.5625000000000002220 ) ) ;
#6130=ORIENTED_EDGE ( 'NONE', *, *, #3353, .T. ) ;
#6133=CARTESIAN_POINT ( 'NONE',  ( -1.500000000000000444, 5.639000000000001123, 0.1250000000000000278 ) ) ;
#6137=EDGE_CURVE ( 'NONE', #3352, #6974, #530, .T. ) ;
#6138=ORIENTED_EDGE ( 'NONE', *, *, #2933, .F. ) ;
#6144=LINE ( 'NONE', #4911, #1917 ) ;
#6151=VERTEX_POINT ( 'NONE', #8178 ) ;
#6153=ADVANCED_FACE ( 'NONE', ( #5775 ), #150, .T. ) ;
#6155=CARTESIAN_POINT ( 'NONE',  ( -2.537500000000000533, 2.500000000000000444, -0.000000000000000000 ) ) ;
#6156=CARTESIAN_POINT ( 'NONE',  ( -3.343750000000001776, 1.750000000000000444, 3.383875000000000632 ) ) ;
#6157=ORIENTED_EDGE ( 'NONE', *, *, #7921, .T. ) ;
#6162=LINE ( 'NONE', #4889, #6070 ) ;
#6163=CARTESIAN_POINT ( 'NONE',  ( -0.7335700379171464780, 2.500000000182677873, -2.750000000000000444 ) ) ;
#6168=FACE_OUTER_BOUND ( 'NONE', #6773, .T. ) ;
#6171=CARTESIAN_POINT ( 'NONE',  ( 3.343750000000002220, 1.750000000000000444, -0.5625000000000003331 ) ) ;
#6177=CARTESIAN_POINT ( 'NONE',  ( -1.625000000000000222, 2.500000000000000000, 2.521780125229002412 ) ) ;
#6181=DIRECTION ( 'NONE',  ( 0.000000000000000000, 1.000000000000000000, 0.000000000000000000 ) ) ;
#6182=ORIENTED_EDGE ( 'NONE', *, *, #333, .F. ) ;
#6189=ORIENTED_EDGE ( 'NONE', *, *, #6835, .T. ) ;
#6190=CARTESIAN_POINT ( 'NONE',  ( 0.000000000000000000, 5.414000000000000590, 0.000000000000000000 ) ) ;
#6192=CIRCLE ( 'NONE', #3046, 3.000000000000000888 ) ;
#6196=ORIENTED_EDGE ( 'NONE', *, *, #7780, .F. ) ;
#6197=ORIENTED_EDGE ( 'NONE', *, *, #1891, .T. ) ;
#6206=VECTOR ( 'NONE', #6362, 39.37007874015748143 ) ;
#6207=CARTESIAN_POINT ( 'NONE',  ( -1.500000000000000444, 5.414000000000000590, 0.1249999999999999445 ) ) ;
#6211=FACE_OUTER_BOUND ( 'NONE', #1134, .T. ) ;
#6212=ORIENTED_EDGE ( 'NONE', *, *, #8098, .T. ) ;
#6218=LINE ( 'NONE', #3111, #5056 ) ;
#6219=DIRECTION ( 'NONE',  ( -0.000000000000000000, 1.000000000000000000, -0.000000000000000000 ) ) ;
#6223=CARTESIAN_POINT ( 'NONE',  ( -3.179822820152304885, 2.000074507124384837, 0.5625000000000001110 ) ) ;
#6232=( BOUNDED_CURVE ( )  B_SPLINE_CURVE ( 2, ( #2872, #2253, #332, #6031, #5995, #996, #5278 ),
 .UNSPECIFIED., .F., .T. ) 
 B_SPLINE_CURVE_WITH_KNOTS ( ( 3, 2, 2, 3 ),
 ( 2.010031869259635242E-11, 0.003869794796933458212, 0.03119827455188316570, 0.05852675430952081204 ),
 .UNSPECIFIED. ) 
 CURVE ( )  GEOMETRIC_REPRESENTATION_ITEM ( )  RATIONAL_B_SPLINE_CURVE ( ( 0.9287967259844018830, 0.9585254409137464737, 1.000000000000000000, 0.7071067811865479058, 1.000000000000000000, 0.7071067811865479058, 1.000000000000000000 ) ) 
 REPRESENTATION_ITEM ( '' )  );
#6234=CARTESIAN_POINT ( 'NONE',  ( -1.500000000000000444, 5.639000000000001123, 0.1249999999999999029 ) ) ;
#6235=AXIS2_PLACEMENT_3D ( 'NONE', #1136, #4898, #7434 ) ;
#6237=DIRECTION ( 'NONE',  ( 0.000000000000000000, 0.000000000000000000, 1.000000000000000000 ) ) ;
#6240=VERTEX_POINT ( 'NONE', #655 ) ;
#6243=CARTESIAN_POINT ( 'NONE',  ( 2.537500000000000533, 1.664000000000000368, 0.000000000000000000 ) ) ;
#6244=CARTESIAN_POINT ( 'NONE',  ( 0.8148948373165970649, 2.920888456407634060, -5.108749999999998792 ) ) ;
#6245=PLANE ( 'NONE',  #8116 ) ;
#6246=ORIENTED_EDGE ( 'NONE', *, *, #5493, .T. ) ;
#6256=CARTESIAN_POINT ( 'NONE',  ( 0.000000000000000000, 3.950000000000000178, -4.308749999765625560 ) ) ;
#6262=CARTESIAN_POINT ( 'NONE',  ( 0.000000000000000000, 3.950000000000000178, 3.691250000234376660 ) ) ;
#6266=ORIENTED_EDGE ( 'NONE', *, *, #5886, .F. ) ;
#6276=ADVANCED_FACE ( 'NONE', ( #5897 ), #4701, .T. ) ;
#6281=EDGE_CURVE ( 'NONE', #1699, #2064, #2161, .T. ) ;
#6284=CARTESIAN_POINT ( 'NONE',  ( 1.270916224172242037, 4.288808537913045171, -5.108750000000001457 ) ) ;
#6290=DIRECTION ( 'NONE',  ( 1.776356839400250465E-15, 0.000000000000000000, -1.000000000000000000 ) ) ;
#6292=ORIENTED_EDGE ( 'NONE', *, *, #5683, .T. ) ;
#6294=EDGE_CURVE ( 'NONE', #6003, #6547, #404, .T. ) ;
#6295=CYLINDRICAL_SURFACE ( 'NONE', #2948, 2.619834094488189269 ) ;
#6298=ORIENTED_EDGE ( 'NONE', *, *, #1919, .F. ) ;
#6299=EDGE_CURVE ( 'NONE', #1844, #5265, #4244, .T. ) ;
#6309=EDGE_LOOP ( 'NONE', ( #2739, #4466, #256, #5094 ) ) ;
#6314=ORIENTED_EDGE ( 'NONE', *, *, #2500, .F. ) ;
#6317=LINE ( 'NONE', #1358, #5305 ) ;
#6318=PLANE ( 'NONE',  #6485 ) ;
#6319=DIRECTION ( 'NONE',  ( -1.000000000000000000, -0.000000000000000000, -0.000000000000000000 ) ) ;
#6322=ORIENTED_EDGE ( 'NONE', *, *, #1694, .F. ) ;
#6326=CARTESIAN_POINT ( 'NONE',  ( 1.267418545190977852, 3.608279822688814420, -5.108750000000002345 ) ) ;
#6331=VECTOR ( 'NONE', #471, 39.37007874015748143 ) ;
#6336=DIRECTION ( 'NONE',  ( 0.000000000000000000, 0.000000000000000000, 1.000000000000000000 ) ) ;
#6343=CARTESIAN_POINT ( 'NONE',  ( 2.750000000000002665, 7.339000000000001300, 3.161250000000001670 ) ) ;
#6345=VECTOR ( 'NONE', #748, 39.37007874015748143 ) ;
#6346=ORIENTED_EDGE ( 'NONE', *, *, #8102, .F. ) ;
#6351=ORIENTED_EDGE ( 'NONE', *, *, #7186, .T. ) ;
#6356=CARTESIAN_POINT ( 'NONE',  ( 0.000000000000000000, 2.500000000000000000, -2.750000000000000444 ) ) ;
#6358=ORIENTED_EDGE ( 'NONE', *, *, #7384, .F. ) ;
#6359=PLANE ( 'NONE',  #227 ) ;
#6362=DIRECTION ( 'NONE',  ( -0.000000000000000000, -0.000000000000000000, 1.000000000000000000 ) ) ;
#6364=ORIENTED_EDGE ( 'NONE', *, *, #2784, .F. ) ;
#6366=CIRCLE ( 'NONE', #2833, 1.249999999999999556 ) ;
#6369=CARTESIAN_POINT ( 'NONE',  ( 1.196592964269871384, 4.489712393535192803, -5.108750000000001457 ) ) ;
#6370=DIRECTION ( 'NONE',  ( 1.000000000000000000, 0.000000000000000000, 0.000000000000000000 ) ) ;
#6374=ORIENTED_EDGE ( 'NONE', *, *, #3639, .T. ) ;
#6375=VECTOR ( 'NONE', #8072, 39.37007874015748143 ) ;
#6378=DIRECTION ( 'NONE',  ( 0.000000000000000000, 0.000000000000000000, -1.000000000000000000 ) ) ;
#6382=FACE_OUTER_BOUND ( 'NONE', #4696, .T. ) ;
#6385=CARTESIAN_POINT ( 'NONE',  ( -1.347488132453362963, 2.365290551065806213, -2.750000000000000444 ) ) ;
#6387=VERTEX_POINT ( 'NONE', #1638 ) ;
#6391=ORIENTED_EDGE ( 'NONE', *, *, #3383, .F. ) ;
#6394=CARTESIAN_POINT ( 'NONE',  ( 1.624999999999999778, 3.950000000000000178, -5.108750000000001457 ) ) ;
#6401=CARTESIAN_POINT ( 'NONE',  ( 0.000000000000000000, 3.950000000000000178, -5.108750000000001457 ) ) ;
#6404=ADVANCED_FACE ( 'NONE', ( #2863 ), #7176, .F. ) ;
#6407=PLANE ( 'NONE',  #2972 ) ;
#6409=ORIENTED_EDGE ( 'NONE', *, *, #2686, .F. ) ;
#6411=CARTESIAN_POINT ( 'NONE',  ( 0.04453716361813374325, 5.262460292302547415, -5.108750000000001457 ) ) ;
#6417=DIRECTION ( 'NONE',  ( 0.000000000000000000, 0.000000000000000000, 1.000000000000000000 ) ) ;
#6418=ORIENTED_EDGE ( 'NONE', *, *, #3383, .T. ) ;
#6426=LINE ( 'NONE', #804, #6512 ) ;
#6427=ORIENTED_EDGE ( 'NONE', *, *, #4079, .F. ) ;
#6432=ORIENTED_EDGE ( 'NONE', *, *, #7681, .F. ) ;
#6433=DIRECTION ( 'NONE',  ( -0.000000000000000000, 1.000000000000000000, 0.000000000000000000 ) ) ;
#6439=VERTEX_POINT ( 'NONE', #7441 ) ;
#6440=ADVANCED_FACE ( 'NONE', ( #1801 ), #2939, .T. ) ;
#6441=DIRECTION ( 'NONE',  ( -0.000000000000000000, -0.000000000000000000, 1.000000000000000000 ) ) ;
#6446=ORIENTED_EDGE ( 'NONE', *, *, #849, .T. ) ;
#6449=ORIENTED_EDGE ( 'NONE', *, *, #2917, .F. ) ;
#6454=AXIS2_PLACEMENT_3D ( 'NONE', #5593, #6985, #7555 ) ;
#6458=VERTEX_POINT ( 'NONE', #6830 ) ;
#6462=CARTESIAN_POINT ( 'NONE',  ( -2.750000000000000444, 7.964000000000000412, 3.323750000000001759 ) ) ;
#6463=DIRECTION ( 'NONE',  ( -1.000000000000000000, 0.000000000000000000, 0.000000000000000000 ) ) ;
#6465=EDGE_LOOP ( 'NONE', ( #5431, #6322, #5960 ) ) ;
#6467=AXIS2_PLACEMENT_3D ( 'NONE', #6190, #7280, #6660 ) ;
#6468=CARTESIAN_POINT ( 'NONE',  ( 1.312500000000000444, 4.908106850393701315, 3.316250000000001474 ) ) ;
#6478=ORIENTED_EDGE ( 'NONE', *, *, #2383, .F. ) ;
#6485=AXIS2_PLACEMENT_3D ( 'NONE', #7279, #3848, #663 ) ;
#6487=DIRECTION ( 'NONE',  ( 0.000000000000000000, -1.000000000000000000, 0.000000000000000000 ) ) ;
#6491=CARTESIAN_POINT ( 'NONE',  ( 2.750000000000000444, 7.339000000000001300, 3.161250000000001670 ) ) ;
#6492=DIRECTION ( 'NONE',  ( -0.000000000000000000, -0.000000000000000000, 1.000000000000000000 ) ) ;
#6495=ORIENTED_EDGE ( 'NONE', *, *, #4589, .T. ) ;
#6496=LINE ( 'NONE', #3368, #1543 ) ;
#6498=EDGE_CURVE ( 'NONE', #5226, #2362, #7521, .T. ) ;
#6499=VECTOR ( 'NONE', #1628, 39.37007874015748143 ) ;
#6505=SHAPE_REPRESENTATION ( 'bench vise2-', ( #7272 ), #2811 ) ;
#6506=ORIENTED_EDGE ( 'NONE', *, *, #2933, .T. ) ;
#6508=VECTOR ( 'NONE', #344, 39.37007874015748143 ) ;
#6512=VECTOR ( 'NONE', #5806, 39.37007874015748143 ) ;
#6513=ORIENTED_EDGE ( 'NONE', *, *, #548, .F. ) ;
#6519=CARTESIAN_POINT ( 'NONE',  ( -1.624999999999999112, 3.950000000000000178, 2.749999999206901968 ) ) ;
#6520=EDGE_CURVE ( 'NONE', #2223, #1240, #6103, .T. ) ;
#6521=CARTESIAN_POINT ( 'NONE',  ( -1.624999999336056877, 2.076218724820237060, -2.750000000000000444 ) ) ;
#6522=CARTESIAN_POINT ( 'NONE',  ( -1.312500000000000444, 4.908106850393701315, 0.5414159055118122899 ) ) ;
#6525=ORIENTED_EDGE ( 'NONE', *, *, #2500, .T. ) ;
#6527=CARTESIAN_POINT ( 'NONE',  ( -1.312500000000000444, 5.414000000000000590, 3.316250000000001474 ) ) ;
#6533=AXIS2_PLACEMENT_3D ( 'NONE', #2589, #2550, #6887 ) ;
#6534=EDGE_LOOP ( 'NONE', ( #597, #7310, #4351, #3559 ) ) ;
#6535=CARTESIAN_POINT ( 'NONE',  ( -1.312363187401233144, 4.037659949503647816, -5.108749999999999680 ) ) ;
#6541=EDGE_LOOP ( 'NONE', ( #3107, #3580, #1347, #5662 ) ) ;
#6547=VERTEX_POINT ( 'NONE', #444 ) ;
#6552=CARTESIAN_POINT ( 'NONE',  ( 0.000000000000000000, 1.750000000000000666, 0.000000000000000000 ) ) ;
#6554=LINE ( 'NONE', #6667, #6508 ) ;
#6556=CARTESIAN_POINT ( 'NONE',  ( 0.000000000000000000, 5.639000000000001123, -2.750000000000000444 ) ) ;
#6564=ORIENTED_EDGE ( 'NONE', *, *, #228, .T. ) ;
#6572=CARTESIAN_POINT ( 'NONE',  ( -1.201750196850394081, 2.500000000000000444, -2.750000000000000444 ) ) ;
#6574=ORIENTED_EDGE ( 'NONE', *, *, #3130, .F. ) ;
#6575=ADVANCED_FACE ( 'NONE', ( #3827 ), #5101, .T. ) ;
#6578=CARTESIAN_POINT ( 'NONE',  ( -1.301660623695976904, 3.780290714801028962, -5.108749999999998792 ) ) ;
#6583=EDGE_LOOP ( 'NONE', ( #5142, #7861, #3090, #321, #5307, #3116, #3818, #7690 ) ) ;
#6584=FACE_OUTER_BOUND ( 'NONE', #4181, .T. ) ;
#6585=DIRECTION ( 'NONE',  ( 0.000000000000000000, 0.000000000000000000, 1.000000000000000000 ) ) ;
#6587=LINE ( 'NONE', #2842, #163 ) ;
#6595=ORIENTED_EDGE ( 'NONE', *, *, #5586, .F. ) ;
#6597=LINE ( 'NONE', #1591, #5292 ) ;
#6607=CARTESIAN_POINT ( 'NONE',  ( 3.343750000000001776, 1.750000000000000444, 3.383875000000000632 ) ) ;
#6609=CARTESIAN_POINT ( 'NONE',  ( 2.537500000000000533, 2.500000000000000444, 0.000000000000000000 ) ) ;
#6615=ORIENTED_EDGE ( 'NONE', *, *, #5095, .T. ) ;
#6616=CARTESIAN_POINT ( 'NONE',  ( 1.312500000123273169, 7.352492868468935683, 3.316250000424603606 ) ) ;
#6618=CARTESIAN_POINT ( 'NONE',  ( -1.242854508572050598, 4.374042214390413186, -5.108749999999998792 ) ) ;
#6619=DIRECTION ( 'NONE',  ( 0.000000000000000000, 0.000000000000000000, -1.000000000000000000 ) ) ;
#6620=AXIS2_PLACEMENT_3D ( 'NONE', #8055, #2390, #3734 ) ;
#6623=VERTEX_POINT ( 'NONE', #800 ) ;
#6626=VECTOR ( 'NONE', #347, 39.37007874015748143 ) ;
#6628=AXIS2_PLACEMENT_3D ( 'NONE', #3753, #642, #7075 ) ;
#6629=DIRECTION ( 'NONE',  ( 0.000000000000000000, 0.000000000000000000, -1.000000000000000000 ) ) ;
#6630=ORIENTED_EDGE ( 'NONE', *, *, #3657, .T. ) ;
#6632=CARTESIAN_POINT ( 'NONE',  ( -0.7335700379171464780, 2.500000000182677873, -2.908930215554831999 ) ) ;
#6634=CARTESIAN_POINT ( 'NONE',  ( -2.537500000000000533, 2.500000000000000444, 0.2625000000000008438 ) ) ;
#6640=VECTOR ( 'NONE', #4539, 39.37007874015748143 ) ;
#6648=VERTEX_POINT ( 'NONE', #3145 ) ;
#6651=LINE ( 'NONE', #5356, #3706 ) ;
#6653=FACE_OUTER_BOUND ( 'NONE', #657, .T. ) ;
#6660=DIRECTION ( 'NONE',  ( 0.000000000000000000, -0.000000000000000000, 1.000000000000000000 ) ) ;
#6665=EDGE_LOOP ( 'NONE', ( #3418, #1292 ) ) ;
#6667=CARTESIAN_POINT ( 'NONE',  ( -1.625000000000000222, 2.500000000000000444, -2.750000000000000444 ) ) ;
#6668=ADVANCED_FACE ( 'NONE', ( #6382 ), #2653, .F. ) ;
#6677=ORIENTED_EDGE ( 'NONE', *, *, #7788, .T. ) ;
#6678=ORIENTED_EDGE ( 'NONE', *, *, #379, .T. ) ;
#6685=FACE_OUTER_BOUND ( 'NONE', #5174, .T. ) ;
#6686=CARTESIAN_POINT ( 'NONE',  ( -0.8651000672161062166, 4.937992838626295011, -5.108750000000002345 ) ) ;
#6712=FACE_OUTER_BOUND ( 'NONE', #5496, .T. ) ;
#6713=EDGE_LOOP ( 'NONE', ( #6314, #1677, #2155, #2291 ) ) ;
#6717=ORIENTED_EDGE ( 'NONE', *, *, #791, .F. ) ;
#6721=LINE ( 'NONE', #4832, #5800 ) ;
#6727=ORIENTED_EDGE ( 'NONE', *, *, #5333, .F. ) ;
#6728=VECTOR ( 'NONE', #3094, 39.37007874015748143 ) ;
#6733=CARTESIAN_POINT ( 'NONE',  ( -3.063407153088590462, 2.250083286718937536, -0.5624999982030005619 ) ) ;
#6737=PLANE ( 'NONE',  #24 ) ;
#6742=DIRECTION ( 'NONE',  ( -1.000000000000000000, -0.000000000000000000, -0.000000000000000000 ) ) ;
#6748=CARTESIAN_POINT ( 'NONE',  ( -1.625000000000000222, 2.500000000077463369, -2.521780125186765975 ) ) ;
#6749=VERTEX_POINT ( 'NONE', #6871 ) ;
#6757=EDGE_LOOP ( 'NONE', ( #1682, #6364, #7888, #6727 ) ) ;
#6766=VERTEX_POINT ( 'NONE', #4727 ) ;
#6768=PLANE ( 'NONE',  #452 ) ;
#6773=EDGE_LOOP ( 'NONE', ( #3942, #5250, #4001, #3075, #4672, #7484, #665, #4338, #4069, #2279 ) ) ;
#6774=DIRECTION ( 'NONE',  ( 0.000000000000000000, 0.000000000000000000, 1.000000000000000000 ) ) ;
#6778=LINE ( 'NONE', #5368, #6061 ) ;
#6782=LINE ( 'NONE', #4767, #3457 ) ;
#6784=VERTEX_POINT ( 'NONE', #3989 ) ;
#6787=EDGE_CURVE ( 'NONE', #2209, #6810, #2851, .T. ) ;
#6788=EDGE_LOOP ( 'NONE', ( #4863, #7890, #3539, #783, #7940, #2736 ) ) ;
#6789=ADVANCED_FACE ( 'NONE', ( #7122 ), #2202, .F. ) ;
#6799=CARTESIAN_POINT ( 'NONE',  ( 1.198957881665148717, 2.500000000196656025, -2.749999999536767437 ) ) ;
#6802=ORIENTED_EDGE ( 'NONE', *, *, #8102, .T. ) ;
#6810=VERTEX_POINT ( 'NONE', #5887 ) ;
#6814=CARTESIAN_POINT ( 'NONE',  ( 0.000000000000000000, 5.113999999999999879, -2.750000000000000444 ) ) ;
#6816=EDGE_LOOP ( 'NONE', ( #5528, #777, #4306, #1254 ) ) ;
#6818=CARTESIAN_POINT ( 'NONE',  ( -1.625000000000000222, 5.639000000000001123, -2.750000000000000444 ) ) ;
#6827=DIRECTION ( 'NONE',  ( -0.000000000000000000, -0.000000000000000000, 1.000000000000000000 ) ) ;
#6828=ORIENTED_EDGE ( 'NONE', *, *, #3732, .F. ) ;
#6830=CARTESIAN_POINT ( 'NONE',  ( -1.312500000000000222, 8.589000000000002188, 3.161250000126027970 ) ) ;
#6831=EDGE_CURVE ( 'NONE', #6974, #2706, #6597, .T. ) ;
#6833=LINE ( 'NONE', #1216, #4274 ) ;
#6835=EDGE_CURVE ( 'NONE', #7577, #2826, #7726, .T. ) ;
#6836=CARTESIAN_POINT ( 'NONE',  ( -1.312500000000000444, 5.414000000000000590, 0.5414159055118118458 ) ) ;
#6838=CARTESIAN_POINT ( 'NONE',  ( -3.343750000000001776, 2.500000000000000444, 0.5625000000000001110 ) ) ;
#6842=CARTESIAN_POINT ( 'NONE',  ( -1.624999999999999778, 3.950000000000000178, 3.691250000234376216 ) ) ;
#6844=ORIENTED_EDGE ( 'NONE', *, *, #1427, .T. ) ;
#6848=DIRECTION ( 'NONE',  ( 0.000000000000000000, 0.000000000000000000, -1.000000000000000000 ) ) ;
#6858=FACE_OUTER_BOUND ( 'NONE', #6583, .T. ) ;
#6859=VERTEX_POINT ( 'NONE', #2239 ) ;
#6862=AXIS2_PLACEMENT_3D ( 'NONE', #1237, #6894, #6933 ) ;
#6868=DIRECTION ( 'NONE',  ( 0.000000000000000000, 0.000000000000000000, -1.000000000000000000 ) ) ;
#6871=CARTESIAN_POINT ( 'NONE',  ( 2.537500000000000533, 1.664000000000000368, -0.2625000000000008438 ) ) ;
#6880=LINE ( 'NONE', #6922, #164 ) ;
#6886=EDGE_CURVE ( 'NONE', #1945, #1578, #4688, .T. ) ;
#6887=DIRECTION ( 'NONE',  ( -1.000000000000000000, 0.000000000000000000, -0.000000000000000000 ) ) ;
#6888=VECTOR ( 'NONE', #4005, 39.37007874015748143 ) ;
#6889=EDGE_CURVE ( 'NONE', #6749, #5733, #2767, .T. ) ;
#6890=EDGE_CURVE ( 'NONE', #4253, #3252, #1549, .T. ) ;
#6892=CARTESIAN_POINT ( 'NONE',  ( 0.000000000000000000, 3.950000000000000178, -2.750000000000000444 ) ) ;
#6894=DIRECTION ( 'NONE',  ( -0.000000000000000000, -0.000000000000000000, 1.000000000000000000 ) ) ;
#6901=CARTESIAN_POINT ( 'NONE',  ( 0.000000000000000000, 2.500000000000000444, -2.749999999536767437 ) ) ;
#6902=CARTESIAN_POINT ( 'NONE',  ( 1.312363190093051912, 3.862340101006792814, -5.108750000000001457 ) ) ;
#6910=LINE ( 'NONE', #3295, #7973 ) ;
#6912=VERTEX_POINT ( 'NONE', #6207 ) ;
#6922=CARTESIAN_POINT ( 'NONE',  ( 1.625000000000000222, 5.113999999999999879, 2.750000000000000444 ) ) ;
#6932=DIRECTION ( 'NONE',  ( 1.000000000000000000, 0.000000000000000000, 0.000000000000000000 ) ) ;
#6933=DIRECTION ( 'NONE',  ( 1.000000000000000000, 0.000000000000000000, 0.000000000000000000 ) ) ;
#6934=CARTESIAN_POINT ( 'NONE',  ( 3.343750000000001776, 1.750000000000000444, 0.5624999982029994516 ) ) ;
#6936=ORIENTED_EDGE ( 'NONE', *, *, #3243, .F. ) ;
#6940=CARTESIAN_POINT ( 'NONE',  ( 1.261644055928290875, 3.587548275720691571, -5.108750000000004121 ) ) ;
#6942=VERTEX_POINT ( 'NONE', #547 ) ;
#6948=LINE ( 'NONE', #5631, #1504 ) ;
#6953=EDGE_CURVE ( 'NONE', #6962, #6912, #6050, .T. ) ;
#6956=EDGE_CURVE ( 'NONE', #4674, #1699, #1710, .T. ) ;
#6958=CARTESIAN_POINT ( 'NONE',  ( 1.312500000000000444, 8.589000000000002188, 3.161250000147724837 ) ) ;
#6962=VERTEX_POINT ( 'NONE', #4233 ) ;
#6970=EDGE_CURVE ( 'NONE', #4298, #7385, #7479, .T. ) ;
#6974=VERTEX_POINT ( 'NONE', #1172 ) ;
#6979=VECTOR ( 'NONE', #412, 39.37007874015748143 ) ;
#6983=CARTESIAN_POINT ( 'NONE',  ( 0.5437243537200630028, 5.145354609571764826, -5.108750000000003233 ) ) ;
#6985=DIRECTION ( 'NONE',  ( -1.000000000000000000, -0.000000000000000000, 0.000000000000000000 ) ) ;
#6986=VERTEX_POINT ( 'NONE', #3670 ) ;
#6989=EDGE_CURVE ( 'NONE', #6648, #4304, #2403, .T. ) ;
#6994=PLANE ( 'NONE',  #6086 ) ;
#6997=CARTESIAN_POINT ( 'NONE',  ( -1.625000000000000222, 2.057992047244095346, 2.750000000000000444 ) ) ;
#6999=VECTOR ( 'NONE', #6319, 39.37007874015748143 ) ;
#7002=ADVANCED_FACE ( 'NONE', ( #6168 ), #5504, .T. ) ;
#7005=DIRECTION ( 'NONE',  ( 1.000000000000000000, 0.000000000000000000, 0.000000000000000000 ) ) ;
#7006=AXIS2_PLACEMENT_3D ( 'NONE', #5512, #488, #1144 ) ;
#7008=ORIENTED_EDGE ( 'NONE', *, *, #5586, .T. ) ;
#7013=EDGE_LOOP ( 'NONE', ( #3658, #2601 ) ) ;
#7018=CARTESIAN_POINT ( 'NONE',  ( 1.312500000000000444, 5.414000000000000590, 2.750000000234376074 ) ) ;
#7019=CARTESIAN_POINT ( 'NONE',  ( 1.312500000000000444, 5.414000000000000590, 3.316250000000001474 ) ) ;
#7027=CIRCLE ( 'NONE', #1404, 1.624999999999999778 ) ;
#7030=CARTESIAN_POINT ( 'NONE',  ( 0.08777339715507348483, 5.260278687702092171, -5.108750000000001457 ) ) ;
#7034=DIRECTION ( 'NONE',  ( -0.000000000000000000, -0.000000000000000000, 1.000000000000000000 ) ) ;
#7036=ORIENTED_EDGE ( 'NONE', *, *, #6498, .T. ) ;
#7037=VECTOR ( 'NONE', #2005, 39.37007874015748143 ) ;
#7038=CYLINDRICAL_SURFACE ( 'NONE', #1651, 0.2625000000000008438 ) ;
#7068=CARTESIAN_POINT ( 'NONE',  ( 3.343750000000002220, 2.500000000000000444, -0.5625000000000003331 ) ) ;
#7075=DIRECTION ( 'NONE',  ( 0.000000000000000000, 0.000000000000000000, 1.000000000000000000 ) ) ;
#7086=DIRECTION ( 'NONE',  ( 1.000000000000000000, 1.681137226870316085E-15, 0.000000000000000000 ) ) ;
#7089=FACE_OUTER_BOUND ( 'NONE', #5426, .T. ) ;
#7093=EDGE_CURVE ( 'NONE', #2271, #6766, #1329, .T. ) ;
#7095=ORIENTED_EDGE ( 'NONE', *, *, #4625, .T. ) ;
#7096=EDGE_CURVE ( 'NONE', #4179, #4253, #4399, .T. ) ;
#7097=CARTESIAN_POINT ( 'NONE',  ( -1.246236536363908742, 3.529356956552051283, -5.108750000000002345 ) ) ;
#7099=CARTESIAN_POINT ( 'NONE',  ( -2.750000000000000444, 7.964000000000000412, 2.411250000000000338 ) ) ;
#7100=LENGTH_MEASURE_WITH_UNIT ( LENGTH_MEASURE( 0.02539999999999999897 ), #7784 );
#7101=DIRECTION ( 'NONE',  ( -0.000000000000000000, -1.000000000000000000, -0.000000000000000000 ) ) ;
#7104=ORIENTED_EDGE ( 'NONE', *, *, #4851, .T. ) ;
#7107=B_SPLINE_CURVE_WITH_KNOTS ( 'NONE', 3,
 ( #6632, #5587, #5658, #37, #1201, #4850, #633, #1165, #2516, #4359, #1737, #4275 ),
 .UNSPECIFIED., .F., .F.,
 ( 4, 2, 2, 2, 2, 4 ),
 ( -0.01980159854141738326, -0.01485119890606303311, -0.009900799270708686428, -0.007425599453031514821, -0.004950399635354338010, 1.040834085586084257E-17 ),
 .UNSPECIFIED. ) ;
#7111=FACE_OUTER_BOUND ( 'NONE', #6541, .T. ) ;
#7115=ORIENTED_EDGE ( 'NONE', *, *, #5767, .T. ) ;
#7122=FACE_OUTER_BOUND ( 'NONE', #7654, .T. ) ;
#7124=CARTESIAN_POINT ( 'NONE',  ( 2.750000000000000444, 8.601289606299213020, 3.691250000000001030 ) ) ;
#7125=VECTOR ( 'NONE', #2320, 39.37007874015748143 ) ;
#7126=ORIENTED_EDGE ( 'NONE', *, *, #2383, .T. ) ;
#7133=VECTOR ( 'NONE', #7622, 39.37007874015748143 ) ;
#7136=VERTEX_POINT ( 'NONE', #5665 ) ;
#7138=CARTESIAN_POINT ( 'NONE',  ( -0.4244989081355610150, 2.705063376247227591, -5.108750000000003233 ) ) ;
#7141=ADVANCED_FACE ( 'NONE', ( #5129 ), #3894, .F. ) ;
#7143=ORIENTED_EDGE ( 'NONE', *, *, #4224, .T. ) ;
#7149=VECTOR ( 'NONE', #7164, 39.37007874015748143 ) ;
#7150=DIRECTION ( 'NONE',  ( -0.000000000000000000, 1.000000000000000000, -0.000000000000000000 ) ) ;
#7151=VECTOR ( 'NONE', #3985, 39.37007874015748143 ) ;
#7155=ORIENTED_EDGE ( 'NONE', *, *, #4966, .T. ) ;
#7156=AXIS2_PLACEMENT_3D ( 'NONE', #3189, #1343, #7086 ) ;
#7157=EDGE_CURVE ( 'NONE', #4596, #277, #3212, .T. ) ;
#7164=DIRECTION ( 'NONE',  ( -0.000000000000000000, 1.000000000000000000, 0.000000000000000000 ) ) ;
#7167=EDGE_CURVE ( 'NONE', #5899, #2271, #5000, .T. ) ;
#7170=PLANE ( 'NONE',  #5047 ) ;
#7172=FACE_OUTER_BOUND ( 'NONE', #1988, .T. ) ;
#7173=DIRECTION ( 'NONE',  ( 0.000000000000000000, 1.000000000000000000, 0.000000000000000000 ) ) ;
#7176=PLANE ( 'NONE',  #328 ) ;
#7178=EDGE_LOOP ( 'NONE', ( #3204, #6677 ) ) ;
#7181=CARTESIAN_POINT ( 'NONE',  ( -1.196592970772699660, 3.410287616584806170, -5.108749999999999680 ) ) ;
#7182=CARTESIAN_POINT ( 'NONE',  ( 0.01493480814038263167, 2.324986238204167943, 3.080221901019060127 ) ) ;
#7183=PLANE ( 'NONE',  #1888 ) ;
#7186=EDGE_CURVE ( 'NONE', #6458, #4928, #1207, .T. ) ;
#7191=PLANE ( 'NONE',  #2538 ) ;
#7197=EDGE_CURVE ( 'NONE', #2439, #7750, #340, .T. ) ;
#7211=LINE ( 'NONE', #5428, #4526 ) ;
#7217=DIRECTION ( 'NONE',  ( 1.000000000000000000, -0.000000000000000000, 0.000000000000000000 ) ) ;
#7222=CARTESIAN_POINT ( 'NONE',  ( -0.8670766215445633307, 2.963758944386602590, -5.108749999999997904 ) ) ;
#7223=CARTESIAN_POINT ( 'NONE',  ( 0.6796442504223291214, 2.472718385001931196, 2.935424685056315486 ) ) ;
#7225=( NAMED_UNIT ( * ) SI_UNIT ( $, .STERADIAN. ) SOLID_ANGLE_UNIT ( ) );
#7228=EDGE_LOOP ( 'NONE', ( #5467, #6506, #6678, #7095, #6802, #4694 ) ) ;
#7238=VERTEX_POINT ( 'NONE', #7756 ) ;
#7240=DIRECTION ( 'NONE',  ( 0.000000000000000000, -0.000000000000000000, 1.000000000000000000 ) ) ;
#7241=CARTESIAN_POINT ( 'NONE',  ( -1.624999999999998446, 3.950000000000000178, 2.749999998413802160 ) ) ;
#7246=DIRECTION ( 'NONE',  ( -0.000000000000000000, 1.000000000000000000, -0.000000000000000000 ) ) ;
#7251=MANIFOLD_SOLID_BREP ( 'Imported1', #5289 ) ;
#7256=VERTEX_POINT ( 'NONE', #265 ) ;
#7258=ORIENTED_EDGE ( 'NONE', *, *, #1919, .T. ) ;
#7263=CARTESIAN_POINT ( 'NONE',  ( -1.624999999371729231, 2.076218724780642511, 2.750000000000000444 ) ) ;
#7265=AXIS2_PLACEMENT_3D ( 'NONE', #6243, #4931, #7470 ) ;
#7266=CARTESIAN_POINT ( 'NONE',  ( 0.000000000000000000, 1.664000000000000368, 2.693920355039552791E-42 ) ) ;
#7267=CARTESIAN_POINT ( 'NONE',  ( -0.2597574076448537772, 2.345571136547101254, 3.059942488945281536 ) ) ;
#7269=DIRECTION ( 'NONE',  ( 0.000000000000000000, 0.000000000000000000, 1.000000000000000000 ) ) ;
#7272=AXIS2_PLACEMENT_3D ( 'NONE', #3736, #6237, #5618 ) ;
#7279=CARTESIAN_POINT ( 'NONE',  ( 0.7335700393700786970, 2.500000000000000444, 2.909883779527559611 ) ) ;
#7280=DIRECTION ( 'NONE',  ( 0.000000000000000000, 1.000000000000000000, 0.000000000000000000 ) ) ;
#7287=ORIENTED_EDGE ( 'NONE', *, *, #333, .T. ) ;
#7288=VECTOR ( 'NONE', #599, 39.37007874015748143 ) ;
#7289=VECTOR ( 'NONE', #7980, 39.37007874015748143 ) ;
#7294=CARTESIAN_POINT ( 'NONE',  ( 0.5069887433553049716, 2.405790110920277503, -3.000813131718135462 ) ) ;
#7296=CARTESIAN_POINT ( 'NONE',  ( -1.625000000000000222, 5.639000000000001123, 0.000000000000000000 ) ) ;
#7297=VERTEX_POINT ( 'NONE', #5455 ) ;
#7306=PLANE ( 'NONE',  #2055 ) ;
#7307=ORIENTED_EDGE ( 'NONE', *, *, #1798, .F. ) ;
#7308=DIRECTION ( 'NONE',  ( 0.000000000000000000, 1.000000000000000000, 0.000000000000000000 ) ) ;
#7310=ORIENTED_EDGE ( 'NONE', *, *, #4040, .T. ) ;
#7318=AXIS2_PLACEMENT_3D ( 'NONE', #4729, #978, #238 ) ;
#7330=ORIENTED_EDGE ( 'NONE', *, *, #7444, .F. ) ;
#7336=CARTESIAN_POINT ( 'NONE',  ( 1.024630039370079126, 4.279065905511812318, -7.087001889763783424 ) ) ;
#7338=VERTEX_POINT ( 'NONE', #7924 ) ;
#7341=DIRECTION ( 'NONE',  ( 0.000000000000000000, -0.000000000000000000, 1.000000000000000000 ) ) ;
#7343=PLANE ( 'NONE',  #2839 ) ;
#7344=FACE_OUTER_BOUND ( 'NONE', #3824, .T. ) ;
#7357=CARTESIAN_POINT ( 'NONE',  ( -1.312500000000000444, 4.908106850393701315, 3.316250000000001474 ) ) ;
#7362=ORIENTED_EDGE ( 'NONE', *, *, #62, .T. ) ;
#7367=LINE ( 'NONE', #6118, #7676 ) ;
#7372=ORIENTED_EDGE ( 'NONE', *, *, #2917, .T. ) ;
#7375=B_SPLINE_CURVE_WITH_KNOTS ( 'NONE', 3,
 ( #6521, #5255, #7813, #6385, #3904, #3941 ),
 .UNSPECIFIED., .F., .F.,
 ( 4, 2, 4 ),
 ( 0.000000000000000000, 0.007631658727031280162, 0.01526331745406256032 ),
 .UNSPECIFIED. ) ;
#7377=CARTESIAN_POINT ( 'NONE',  ( -0.9761938188976380104, 4.405876181102362565, -7.086507244094490510 ) ) ;
#7379=CARTESIAN_POINT ( 'NONE',  ( -1.625000000000000222, 2.359134605132341189, -2.598586947523131574 ) ) ;
#7384=EDGE_CURVE ( 'NONE', #6810, #2355, #6778, .T. ) ;
#7385=VERTEX_POINT ( 'NONE', #1656 ) ;
#7386=DIRECTION ( 'NONE',  ( 0.000000000000000000, 1.000000000000000000, 0.000000000000000000 ) ) ;
#7393=CARTESIAN_POINT ( 'NONE',  ( -0.4206575637829014225, 5.194009207123433391, -5.108750000000004121 ) ) ;
#7396=AXIS2_PLACEMENT_3D ( 'NONE', #7266, #1526, #5234 ) ;
#7404=LINE ( 'NONE', #4257, #883 ) ;
#7406=ORIENTED_EDGE ( 'NONE', *, *, #7910, .T. ) ;
#7407=VECTOR ( 'NONE', #4312, 39.37007874015748143 ) ;
#7414=DIRECTION ( 'NONE',  ( -0.000000000000000000, 1.000000000000000000, -0.000000000000000000 ) ) ;
#7416=DIRECTION ( 'NONE',  ( 0.000000000000000000, -0.000000000000000000, 1.000000000000000000 ) ) ;
#7418=EDGE_LOOP ( 'NONE', ( #4115, #1062, #478 ) ) ;
#7430=DIRECTION ( 'NONE',  ( -1.000000000000000000, 0.000000000000000000, -0.000000000000000000 ) ) ;
#7432=EDGE_LOOP ( 'NONE', ( #283, #1691, #6615, #961 ) ) ;
#7434=DIRECTION ( 'NONE',  ( 1.000000000000000000, 0.000000000000000000, -0.000000000000000000 ) ) ;
#7435=ADVANCED_FACE ( 'NONE', ( #6121 ), #6737, .T. ) ;
#7436=ORIENTED_EDGE ( 'NONE', *, *, #4927, .F. ) ;
#7437=VECTOR ( 'NONE', #477, 39.37007874015748143 ) ;
#7439=ORIENTED_EDGE ( 'NONE', *, *, #5493, .F. ) ;
#7441=CARTESIAN_POINT ( 'NONE',  ( -2.537500000000000533, 2.500000000000000444, 0.2625000000000008438 ) ) ;
#7444=EDGE_CURVE ( 'NONE', #4731, #6648, #6192, .T. ) ;
#7449=DIRECTION ( 'NONE',  ( -0.000000000000000000, -0.000000000000000000, -1.000000000000000000 ) ) ;
#7450=DIRECTION ( 'NONE',  ( 1.000000000000000000, 0.000000000000000000, 0.000000000000000000 ) ) ;
#7455=CARTESIAN_POINT ( 'NONE',  ( 0.000000000000000000, 5.113999999999999879, -2.750000000000000444 ) ) ;
#7456=AXIS2_PLACEMENT_3D ( 'NONE', #91, #131, #2648 ) ;
#7461=ORIENTED_EDGE ( 'NONE', *, *, #887, .F. ) ;
#7462=AXIS2_PLACEMENT_3D ( 'NONE', #1969, #1887, #23 ) ;
#7468=EDGE_LOOP ( 'NONE', ( #5664, #2248, #5756, #5391 ) ) ;
#7470=DIRECTION ( 'NONE',  ( 0.000000000000000000, 0.000000000000000000, 1.000000000000000000 ) ) ;
#7473=CARTESIAN_POINT ( 'NONE',  ( 1.500000000000000444, 5.414000000000000590, -2.750000000000000444 ) ) ;
#7476=ORIENTED_EDGE ( 'NONE', *, *, #2684, .T. ) ;
#7479=LINE ( 'NONE', #514, #7288 ) ;
#7480=EDGE_CURVE ( 'NONE', #2826, #3433, #6880, .T. ) ;
#7483=LINE ( 'NONE', #604, #6375 ) ;
#7484=ORIENTED_EDGE ( 'NONE', *, *, #791, .T. ) ;
#7495=LINE ( 'NONE', #4993, #2808 ) ;
#7506=ORIENTED_EDGE ( 'NONE', *, *, #7524, .F. ) ;
#7508=LINE ( 'NONE', #6901, #974 ) ;
#7510=CARTESIAN_POINT ( 'NONE',  ( -0.8694070078740159246, 2.427999212598427103, -5.651320433070869953 ) ) ;
#7511=CARTESIAN_POINT ( 'NONE',  ( 0.000000000000000000, 5.414000000000000590, 0.1250000000000000278 ) ) ;
#7512=ORIENTED_EDGE ( 'NONE', *, *, #1955, .T. ) ;
#7514=DIRECTION ( 'NONE',  ( 0.000000000000000000, 0.000000000000000000, 1.000000000000000000 ) ) ;
#7515=ORIENTED_EDGE ( 'NONE', *, *, #3280, .F. ) ;
#7519=VERTEX_POINT ( 'NONE', #8130 ) ;
#7521=LINE ( 'NONE', #1214, #1639 ) ;
#7524=EDGE_CURVE ( 'NONE', #1240, #7663, #4297, .T. ) ;
#7527=EDGE_CURVE ( 'NONE', #1578, #4491, #5394, .T. ) ;
#7534=EDGE_LOOP ( 'NONE', ( #3816, #6418, #793, #6351, #7476, #3953, #1978 ) ) ;
#7539=CYLINDRICAL_SURFACE ( 'NONE', #6620, 0.2625000000000008438 ) ;
#7541=AXIS2_PLACEMENT_3D ( 'NONE', #592, #3630, #4394 ) ;
#7542=FACE_OUTER_BOUND ( 'NONE', #6060, .T. ) ;
#7544=ORIENTED_EDGE ( 'NONE', *, *, #2725, .F. ) ;
#7545=VERTEX_POINT ( 'NONE', #4989 ) ;
#7549=CARTESIAN_POINT ( 'NONE',  ( 1.277972679321882632, 3.650152906200382130, -5.108750000000001457 ) ) ;
#7555=DIRECTION ( 'NONE',  ( 0.000000000000000000, 0.000000000000000000, 1.000000000000000000 ) ) ;
#7561=CARTESIAN_POINT ( 'NONE',  ( -2.749999999999999556, 7.964000000000000412, 2.411250000000000338 ) ) ;
#7568=VECTOR ( 'NONE', #7246, 39.37007874015748143 ) ;
#7569=CARTESIAN_POINT ( 'NONE',  ( -1.198957880909643725, 2.499999999928966599, 2.750000000000000444 ) ) ;
#7577=VERTEX_POINT ( 'NONE', #1222 ) ;
#7580=( BOUNDED_CURVE ( )  B_SPLINE_CURVE ( 2, ( #3754, #5060, #2526, #7599, #7561, #1907, #5846, #5214, #7722 ),
 .UNSPECIFIED., .F., .F. ) 
 B_SPLINE_CURVE_WITH_KNOTS ( ( 3, 2, 2, 2, 3 ),
 ( 0.000000000000000000, 0.01376350590101864911, 0.04131120848487213754, 0.06885891106872543688, 0.07294458654364180394 ),
 .UNSPECIFIED. ) 
 CURVE ( )  GEOMETRIC_REPRESENTATION_ITEM ( )  RATIONAL_B_SPLINE_CURVE ( ( 0.8535534732088591037, 0.8536633850130519452, 1.000000000000000000, 0.7071067811865479058, 1.000000000000000000, 0.7071067811865479058, 1.000000000000000000, 0.9565602018087399072, 0.9260057553135151442 ) ) 
 REPRESENTATION_ITEM ( '' )  );
#7583=AXIS2_PLACEMENT_3D ( 'NONE', #6892, #1849, #7620 ) ;
#7586=VERTEX_POINT ( 'NONE', #614 ) ;
#7590=CARTESIAN_POINT ( 'NONE',  ( 1.113928741201104078, 3.255531826294225883, -5.108750000000003233 ) ) ;
#7595=CARTESIAN_POINT ( 'NONE',  ( 1.198957881890679422, 2.500000000000000000, 2.749999999536767437 ) ) ;
#7598=DIRECTION ( 'NONE',  ( 0.000000000000000000, -1.000000000000000000, 0.000000000000000000 ) ) ;
#7599=CARTESIAN_POINT ( 'NONE',  ( -2.749999999999998668, 7.339000000000003077, 2.411250000000000782 ) ) ;
#7609=ORIENTED_EDGE ( 'NONE', *, *, #1798, .T. ) ;
#7611=CARTESIAN_POINT ( 'NONE',  ( -2.750000000000000444, 7.541160346212514298, 3.714531354832316445 ) ) ;
#7620=DIRECTION ( 'NONE',  ( 1.000000000000000000, 0.000000000000000000, 0.000000000000000000 ) ) ;
#7621=LINE ( 'NONE', #3202, #1505 ) ;
#7622=DIRECTION ( 'NONE',  ( -1.000000000000000000, -0.000000000000000000, -0.000000000000000000 ) ) ;
#7629=CARTESIAN_POINT ( 'NONE',  ( 1.116010524871317244, 4.642101986333586616, -5.108750000000002345 ) ) ;
#7634=EDGE_CURVE ( 'NONE', #6439, #7338, #7806, .T. ) ;
#7636=DIRECTION ( 'NONE',  ( -0.000000000000000000, 1.000000000000000000, -0.000000000000000000 ) ) ;
#7644=ORIENTED_EDGE ( 'NONE', *, *, #830, .T. ) ;
#7647=DIRECTION ( 'NONE',  ( -0.000000000000000000, 1.000000000000000000, -0.000000000000000000 ) ) ;
#7652=LINE ( 'NONE', #4619, #3622 ) ;
#7654=EDGE_LOOP ( 'NONE', ( #3531, #6409, #5668, #6574, #2495, #4434, #1155 ) ) ;
#7663=VERTEX_POINT ( 'NONE', #5109 ) ;
#7667=CARTESIAN_POINT ( 'NONE',  ( 0.7665824091426678422, 5.016224573579987300, -5.108750000000005009 ) ) ;
#7676=VECTOR ( 'NONE', #4961, 39.37007874015748143 ) ;
#7678=DIRECTION ( 'NONE',  ( 0.000000000000000000, 0.000000000000000000, 1.000000000000000000 ) ) ;
#7679=LINE ( 'NONE', #1950, #1113 ) ;
#7681=EDGE_CURVE ( 'NONE', #4377, #843, #5499, .T. ) ;
#7687=DIRECTION ( 'NONE',  ( 0.000000000000000000, -1.000000000000000000, 0.000000000000000000 ) ) ;
#7690=ORIENTED_EDGE ( 'NONE', *, *, #5505, .T. ) ;
#7696=CARTESIAN_POINT ( 'NONE',  ( -1.500000000000000444, 5.639000000000001123, -2.750000000000000444 ) ) ;
#7704=AXIS2_PLACEMENT_3D ( 'NONE', #356, #2531, #8035 ) ;
#7713=CARTESIAN_POINT ( 'NONE',  ( 0.9907400445861593852, 4.815212283617434252, -5.108749999999999680 ) ) ;
#7721=CARTESIAN_POINT ( 'NONE',  ( 2.537500000000000533, 2.500000000000000444, 0.000000000000000000 ) ) ;
#7722=CARTESIAN_POINT ( 'NONE',  ( -2.750000000000000444, 8.574153543306394454, 3.323750000003751648 ) ) ;
#7725=EDGE_CURVE ( 'NONE', #2362, #3476, #1369, .T. ) ;
#7726=LINE ( 'NONE', #3469, #7149 ) ;
#7736=ORIENTED_EDGE ( 'NONE', *, *, #4387, .T. ) ;
#7745=LINE ( 'NONE', #2097, #6206 ) ;
#7746=CARTESIAN_POINT ( 'NONE',  ( 2.750000000000000444, 7.964000000000000412, 2.411250000000000338 ) ) ;
#7747=LINE ( 'NONE', #2715, #6999 ) ;
#7750=VERTEX_POINT ( 'NONE', #6163 ) ;
#7756=CARTESIAN_POINT ( 'NONE',  ( 1.500000000000000444, 5.414000000000000590, 0.1249999999999999861 ) ) ;
#7767=ADVANCED_FACE ( 'N', ( #4812 ), #3407, .T. ) ;
#7769=DIRECTION ( 'NONE',  ( -0.000000000000000000, -0.000000000000000000, 1.000000000000000000 ) ) ;
#7771=ORIENTED_EDGE ( 'NONE', *, *, #249, .T. ) ;
#7779=ORIENTED_EDGE ( 'NONE', *, *, #62, .F. ) ;
#7780=EDGE_CURVE ( 'NONE', #5858, #3252, #4186, .T. ) ;
#7782=CARTESIAN_POINT ( 'NONE',  ( -0.5437243662217851048, 2.754645391114584729, -5.108750000000005009 ) ) ;
#7783=CARTESIAN_POINT ( 'NONE',  ( 0.7335700384228724946, 2.500000000438529657, -5.108750000000001457 ) ) ;
#7784=( LENGTH_UNIT ( ) NAMED_UNIT ( * ) SI_UNIT ( $, .METRE. ) );
#7786=ORIENTED_EDGE ( 'NONE', *, *, #279, .T. ) ;
#7788=EDGE_CURVE ( 'NONE', #95, #6942, #3560, .T. ) ;
#7790=DIRECTION ( 'NONE',  ( -0.000000000000000000, 1.000000000000000000, -0.000000000000000000 ) ) ;
#7795=DIRECTION ( 'NONE',  ( 1.000000000000000000, -0.000000000000000000, -0.000000000000000000 ) ) ;
#7797=ADVANCED_FACE ( 'NONE', ( #5170 ), #1540, .T. ) ;
#7801=AXIS2_PLACEMENT_3D ( 'NONE', #6552, #130, #1050 ) ;
#7803=CARTESIAN_POINT ( 'NONE',  ( 1.198957881665148717, 2.500000000196656025, -2.749999999536767437 ) ) ;
#7804=CARTESIAN_POINT ( 'NONE',  ( 0.2593509847069561114, 2.344531234934315478, -3.060965062716212159 ) ) ;
#7806=CIRCLE ( 'NONE', #1874, 0.2625000000000008438 ) ;
#7813=CARTESIAN_POINT ( 'NONE',  ( -1.489119986650662364, 2.223645902236881966, -2.750000000000000444 ) ) ;
#7819=EDGE_LOOP ( 'NONE', ( #4132, #3035 ) ) ;
#7828=CARTESIAN_POINT ( 'NONE',  ( -0.001186137648316157355, 2.637500537863615158, -5.108750000000001457 ) ) ;
#7830=FACE_OUTER_BOUND ( 'NONE', #1672, .T. ) ;
#7831=CARTESIAN_POINT ( 'NONE',  ( 2.750000000000000444, 7.338999999999999524, 3.471636850393701401 ) ) ;
#7834=ORIENTED_EDGE ( 'NONE', *, *, #7480, .F. ) ;
#7838=AXIS2_PLACEMENT_3D ( 'NONE', #6997, #682, #764 ) ;
#7839=AXIS2_PLACEMENT_3D ( 'NONE', #5917, #884, #306 ) ;
#7842=CARTESIAN_POINT ( 'NONE',  ( 0.000000000000000000, 5.113999999999999879, 0.000000000000000000 ) ) ;
#7845=ORIENTED_EDGE ( 'NONE', *, *, #2768, .F. ) ;
#7847=APPLICATION_CONTEXT ( 'configuration controlled 3d designs of mechanical parts and assemblies' ) ;
#7861=ORIENTED_EDGE ( 'NONE', *, *, #1245, .T. ) ;
#7868=VERTEX_POINT ( 'NONE', #7068 ) ;
#7874=CARTESIAN_POINT ( 'NONE',  ( -0.1740164513111777667, 2.648365384722445093, -5.108749999999999680 ) ) ;
#7875=CARTESIAN_POINT ( 'NONE',  ( -0.1316627106748616272, 2.329054901387897836, 3.076208900215326114 ) ) ;
#7877=CARTESIAN_POINT ( 'NONE',  ( -1.312500000000000444, 7.352492874015749358, 3.316250000000001474 ) ) ;
#7883=EDGE_CURVE ( 'NONE', #1240, #7297, #6587, .T. ) ;
#7888=ORIENTED_EDGE ( 'NONE', *, *, #1584, .F. ) ;
#7889=DIRECTION ( 'NONE',  ( -0.000000000000000000, -0.000000000000000000, 1.000000000000000000 ) ) ;
#7890=ORIENTED_EDGE ( 'NONE', *, *, #2991, .F. ) ;
#7891=CARTESIAN_POINT ( 'NONE',  ( -1.644500000000000739, 2.305500000000000771, -5.108750000000001457 ) ) ;
#7894=FACE_OUTER_BOUND ( 'NONE', #3517, .T. ) ;
#7903=ORIENTED_EDGE ( 'NONE', *, *, #8114, .F. ) ;
#7904=DIRECTION ( 'NONE',  ( -0.000000000000000000, 0.000000000000000000, 1.000000000000000000 ) ) ;
#7910=EDGE_CURVE ( 'NONE', #6912, #6003, #4093, .T. ) ;
#7912=CARTESIAN_POINT ( 'NONE',  ( -2.750000000000000444, 7.964000000000001300, 3.691250000000001030 ) ) ;
#7913=CARTESIAN_POINT ( 'NONE',  ( -1.277972681119055709, 4.249847095080741433, -5.108750000000003233 ) ) ;
#7914=CARTESIAN_POINT ( 'NONE',  ( -0.7335700375402988138, 2.499999999992026378, 2.908930215739981229 ) ) ;
#7915=FACE_OUTER_BOUND ( 'NONE', #6713, .T. ) ;
#7918=ORIENTED_EDGE ( 'NONE', *, *, #7883, .F. ) ;
#7921=EDGE_CURVE ( 'NONE', #7136, #1059, #5877, .T. ) ;
#7922=FACE_OUTER_BOUND ( 'NONE', #7534, .T. ) ;
#7923=DIRECTION ( 'NONE',  ( 0.000000000000000000, 1.000000000000000000, -0.000000000000000000 ) ) ;
#7924=CARTESIAN_POINT ( 'NONE',  ( -2.537500000000000533, 2.500000000000000444, -0.2625000000000008438 ) ) ;
#7927=LINE ( 'NONE', #1703, #744 ) ;
#7931=LINE ( 'NONE', #6634, #3709 ) ;
#7938=EDGE_CURVE ( 'NONE', #2826, #4397, #1044, .T. ) ;
#7940=ORIENTED_EDGE ( 'NONE', *, *, #113, .F. ) ;
#7941=VECTOR ( 'NONE', #7795, 39.37007874015748143 ) ;
#7942=AXIS2_PLACEMENT_3D ( 'NONE', #7124, #2770, #5182 ) ;
#7950=EDGE_LOOP ( 'NONE', ( #5730, #5238 ) ) ;
#7956=FACE_OUTER_BOUND ( 'NONE', #3284, .T. ) ;
#7965=VECTOR ( 'NONE', #2415, 39.37007874015748143 ) ;
#7967=VECTOR ( 'NONE', #7308, 39.37007874015748143 ) ;
#7969=PLANE ( 'NONE',  #1889 ) ;
#7973=VECTOR ( 'NONE', #796, 39.37007874015748143 ) ;
#7977=DIRECTION ( 'NONE',  ( -1.000000000000000000, -0.000000000000000000, -0.000000000000000000 ) ) ;
#7979=DIRECTION ( 'NONE',  ( 0.000000000000000000, 0.000000000000000000, -1.000000000000000000 ) ) ;
#7980=DIRECTION ( 'NONE',  ( 0.000000000000000000, -0.000000000000000000, 1.000000000000000000 ) ) ;
#7989=VECTOR ( 'NONE', #4493, 39.37007874015748143 ) ;
#8000=ORIENTED_EDGE ( 'NONE', *, *, #2991, .T. ) ;
#8001=DIRECTION ( 'NONE',  ( -0.000000000000000000, -1.000000000000000000, -0.000000000000000000 ) ) ;
#8002=CIRCLE ( 'NONE', #2321, 3.000000000000000888 ) ;
#8003=AXIS2_PLACEMENT_3D ( 'NONE', #2755, #7790, #2795 ) ;
#8004=CARTESIAN_POINT ( 'NONE',  ( -1.889618362131626726E-10, 5.113999999999999879, 2.750000000234376074 ) ) ;
#8005=CARTESIAN_POINT ( 'NONE',  ( 0.4152326938056751793, 2.378623393394907026, 3.027452056815282955 ) ) ;
#8011=EDGE_CURVE ( 'NONE', #266, #4928, #3032, .T. ) ;
#8013=DIRECTION ( 'NONE',  ( -0.000000000000000000, 1.000000000000000000, 0.000000000000000000 ) ) ;
#8014=CARTESIAN_POINT ( 'NONE',  ( -1.500000000000000444, 5.113999999999999879, 0.1249999999999999029 ) ) ;
#8021=CARTESIAN_POINT ( 'NONE',  ( -3.296097361031207207, 1.750000000037170489, -0.5624999991015005030 ) ) ;
#8023=DIRECTION ( 'NONE',  ( 0.000000000000000000, 0.000000000000000000, -1.000000000000000000 ) ) ;
#8024=VERTEX_POINT ( 'NONE', #1777 ) ;
#8026=DIRECTION ( 'NONE',  ( -0.000000000000000000, -0.000000000000000000, 1.000000000000000000 ) ) ;
#8028=EDGE_LOOP ( 'NONE', ( #6130, #7834, #4735, #7512 ) ) ;
#8035=DIRECTION ( 'NONE',  ( 0.000000000000000000, 0.000000000000000000, 1.000000000000000000 ) ) ;
#8043=DIRECTION ( 'NONE',  ( -0.000000000000000000, 0.000000000000000000, 1.000000000000000000 ) ) ;
#8055=CARTESIAN_POINT ( 'NONE',  ( -2.537500000000000533, 2.500000000000000444, -0.000000000000000000 ) ) ;
#8062=ADVANCED_FACE ( 'NONE', ( #2994, #3695 ), #7969, .F. ) ;
#8063=CARTESIAN_POINT ( 'NONE',  ( -1.356031417322835608, 5.217694212598425807, -5.293171771653544688 ) ) ;
#8065=DIRECTION ( 'NONE',  ( 0.000000000000000000, -1.000000000000000000, 0.000000000000000000 ) ) ;
#8070=CARTESIAN_POINT ( 'NONE',  ( 2.750000000000000000, 7.521783347043602852, 3.691250000474206150 ) ) ;
#8072=DIRECTION ( 'NONE',  ( -0.000000000000000000, -1.000000000000000000, -0.000000000000000000 ) ) ;
#8073=ORIENTED_EDGE ( 'NONE', *, *, #3582, .F. ) ;
#8093=CIRCLE ( 'NONE', #7265, 0.2625000000000008438 ) ;
#8096=AXIS2_PLACEMENT_3D ( 'NONE', #3041, #7979, #8110 ) ;
#8097=EDGE_LOOP ( 'NONE', ( #910, #1588, #3524, #3968, #7439, #7918, #3925, #2821, #6936 ) ) ;
#8098=EDGE_CURVE ( 'NONE', #1286, #1721, #1767, .T. ) ;
#8099=AXIS2_PLACEMENT_3D ( 'NONE', #4463, #5824, #207 ) ;
#8102=EDGE_CURVE ( 'NONE', #6859, #7256, #7621, .T. ) ;
#8103=EDGE_LOOP ( 'NONE', ( #2514, #4845 ) ) ;
#8110=DIRECTION ( 'NONE',  ( 1.000000000000000000, -1.681137231067760553E-15, 0.000000000000000000 ) ) ;
#8111=ORIENTED_EDGE ( 'NONE', *, *, #3833, .T. ) ;
#8114=EDGE_CURVE ( 'NONE', #4495, #6784, #3808, .T. ) ;
#8115=ADVANCED_FACE ( 'NONE', ( #7542 ), #6318, .T. ) ;
#8116=AXIS2_PLACEMENT_3D ( 'NONE', #2451, #3079, #1856 ) ;
#8118=ORIENTED_EDGE ( 'NONE', *, *, #2634, .F. ) ;
#8126=AXIS2_PLACEMENT_3D ( 'NONE', #2045, #3909, #807 ) ;
#8129=PLANE ( 'NONE',  #2184 ) ;
#8130=CARTESIAN_POINT ( 'NONE',  ( 3.296097360936645959, 1.749999999910763826, -0.5625000000000002220 ) ) ;
#8133=EDGE_CURVE ( 'NONE', #7256, #4377, #5042, .T. ) ;
#8137=PLANE ( 'NONE',  #6533 ) ;
#8140=AXIS2_PLACEMENT_3D ( 'NONE', #6234, #5614, #4461 ) ;
#8141=PLANE ( 'NONE',  #6467 ) ;
#8142=CARTESIAN_POINT ( 'NONE',  ( 0.7335700379894659617, 2.500000000219264606, 2.749999999536766992 ) ) ;
#8145=ORIENTED_EDGE ( 'NONE', *, *, #6956, .F. ) ;
#8146=VERTEX_POINT ( 'NONE', #1361 ) ;
#8147=B_SPLINE_CURVE_WITH_KNOTS ( 'NONE', 3,
 ( #536, #5617, #6733, #1816 ),
 .UNSPECIFIED., .F., .F.,
 ( 4, 4 ),
 ( 6.031472751832138938E-13, 0.02101476597407635552 ),
 .UNSPECIFIED. ) ;
#8150=CARTESIAN_POINT ( 'NONE',  ( 0.1355816141732284208, 5.291204763779528086, -5.034844055118110617 ) ) ;
#8152=ORIENTED_EDGE ( 'NONE', *, *, #4976, .T. ) ;
#8157=ORIENTED_EDGE ( 'NONE', *, *, #6890, .F. ) ;
#8162=CARTESIAN_POINT ( 'NONE',  ( 1.625000000000000222, 2.499999999434268982, 2.521780125537467665 ) ) ;
#8167=CARTESIAN_POINT ( 'NONE',  ( -1.624999999999998890, 5.113999999999999879, 2.749999998942535218 ) ) ;
#8168=CARTESIAN_POINT ( 'NONE',  ( -1.198957880909643725, 2.499999999928966599, 2.750000000000000444 ) ) ;
#8174=ORIENTED_EDGE ( 'NONE', *, *, #2731, .F. ) ;
#8178=CARTESIAN_POINT ( 'NONE',  ( 3.343750000000002220, 1.750000000000000444, 0.5624999982029994516 ) ) ;
#8180=ORIENTED_EDGE ( 'NONE', *, *, #4977, .F. ) ;
#8181=CARTESIAN_POINT ( 'NONE',  ( 3.479221556377631263E-16, 1.750000000000000444, -2.841000000000000636 ) ) ;
#8206=COLOUR_RGB('Light Blue', 0.31764706, 0.68627451, 0.89019608);
#8207=FILL_AREA_STYLE_COLOUR('',#8206);
#8208=FILL_AREA_STYLE('',(#8207));
#8209=SURFACE_STYLE_FILL_AREA(#8208);
#8210=SURFACE_SIDE_STYLE('',(#8209));
#8211=SURFACE_STYLE_USAGE(.BOTH.,#8210);
#8212=PRESENTATION_STYLE_ASSIGNMENT((#8211));
#8253=STYLED_ITEM('',(#8212),#7251);
#8254=MECHANICAL_DESIGN_GEOMETRIC_PRESENTATION_REPRESENTATION('',(#8253),#2811);
ENDSEC;
END-ISO-10303-21;
